ISO-10303-21;
HEADER;
FILE_DESCRIPTION (('STEP AP214'),
    '1' );
FILE_NAME ('Snap Open Cable Crossbars 8.step',
    '2026-10-08T22:59:04',
    ( '' ),
    ( '' ),
    'SwSTEP 2.0',
    'SolidWorks 2020',
    '' );
FILE_SCHEMA (( 'AUTOMOTIVE_DESIGN' ));
ENDSEC;

DATA;
#18=CARTESIAN_POINT ( 'NONE',  ( -17.29838795460356593, 22.07107181154411890, -229.9709893146081754 ) ) ;
#113=VERTEX_POINT ( 'NONE', #246350 ) ;
#295=VERTEX_POINT ( 'NONE', #252749 ) ;
#342=EDGE_CURVE ( 'NONE', #84120, #176836, #119484, .T. ) ;
#438=ADVANCED_FACE ( 'NONE', ( #220054 ), #102639, .T. ) ;
#462=CARTESIAN_POINT ( 'NONE',  ( -16.77180007708461318, 22.96538637364528412, -230.9282705005597620 ) ) ;
#464=CARTESIAN_POINT ( 'NONE',  ( -15.55912972643740488, 29.51733789627897409, -236.0932609367895907 ) ) ;
#532=LINE ( 'NONE', #140035, #145210 ) ;
#568=CARTESIAN_POINT ( 'NONE',  ( 18.39999999999999503, 32.67104411594546320, -237.4063322638886859 ) ) ;
#590=CARTESIAN_POINT ( 'NONE',  ( -18.40000000000000213, 23.63051550414076729, -229.7170656735756324 ) ) ;
#701=CARTESIAN_POINT ( 'NONE',  ( 16.87683809663750267, 22.97806745954241592, -230.9350634111226270 ) ) ;
#787=CARTESIAN_POINT ( 'NONE',  ( -14.56336952470179824, 27.81851053932208728, -234.0989799278904115 ) ) ;
#894=FACE_OUTER_BOUND ( 'NONE', #91992, .T. ) ;
#923=ORIENTED_EDGE ( 'NONE', *, *, #9294, .F. ) ;
#1178=CARTESIAN_POINT ( 'NONE',  ( -16.94333152882355975, 30.26242836586778040, -234.7913307026829841 ) ) ;
#1188=CARTESIAN_POINT ( 'NONE',  ( -16.87665923198281348, 30.20632856012693424, -234.8070450048000737 ) ) ;
#1633=ADVANCED_BREP_SHAPE_REPRESENTATION ( '', ( #20540, #2425 ), #56573 ) ;
#1664=SURFACE_SIDE_STYLE ('',( #16137 ) ) ;
#1751=( BOUNDED_CURVE ( )  B_SPLINE_CURVE ( 3, ( #102851, #178596, #160316, #198125 ),
 .UNSPECIFIED., .F., .T. ) 
 B_SPLINE_CURVE_WITH_KNOTS ( ( 4, 4 ),
 ( 1.570796326794904108, 3.141592653589698969 ),
 .UNSPECIFIED. ) 
 CURVE ( )  GEOMETRIC_REPRESENTATION_ITEM ( )  RATIONAL_B_SPLINE_CURVE ( ( 1.000000000000000000, 0.8047378541243889183, 0.8047378541243889183, 1.000000000000000000 ) ) 
 REPRESENTATION_ITEM ( '' )  );
#1795=ORIENTED_EDGE ( 'NONE', *, *, #173721, .T. ) ;
#1804=SHAPE_REPRESENTATION ( 'Snap Open Cable Crossbars 8', ( #2425 ), #56573 ) ;
#1982=ORIENTED_EDGE ( 'NONE', *, *, #257181, .F. ) ;
#2425=AXIS2_PLACEMENT_3D ( 'NONE', #153513, #135160, #16531 ) ;
#2556=ORIENTED_EDGE ( 'NONE', *, *, #177322, .F. ) ;
#2595=AXIS2_PLACEMENT_3D ( 'NONE', #95829, #133693, #234071 ) ;
#2733=VECTOR ( 'NONE', #35224, 1000.000000000000000 ) ;
#2814=DIRECTION ( 'NONE',  ( 0.000000000000000000, 0.4721928772777346239, 0.8814952561688430555 ) ) ;
#2870=CARTESIAN_POINT ( 'NONE',  ( -16.77779411440718249, 30.19297764007214724, -234.8043159413754211 ) ) ;
#3094=CARTESIAN_POINT ( 'NONE',  ( -16.87683809663752754, 29.61458345175765317, -234.5865886027308136 ) ) ;
#3126=CARTESIAN_POINT ( 'NONE',  ( -16.89268316805465986, 30.21221237062500720, -234.8082435139909592 ) ) ;
#3208=DIRECTION ( 'NONE',  ( -1.000000000000000000, 0.000000000000000000, 0.000000000000000000 ) ) ;
#3369=CARTESIAN_POINT ( 'NONE',  ( -13.54036565897076194, 27.85878770204270793, -234.1150007431636766 ) ) ;
#3537=CARTESIAN_POINT ( 'NONE',  ( -16.97683809663752186, 29.49590395944697718, -234.5399335999045718 ) ) ;
#3571=ORIENTED_EDGE ( 'NONE', *, *, #196703, .F. ) ;
#3746=B_SPLINE_CURVE_WITH_KNOTS ( 'NONE', 3,
 ( #178586, #79433, #1178, #119892, #145509, #67264, #19492, #146776, #39066, #225032, #124681, #97699, #204200 ),
 .UNSPECIFIED., .F., .F.,
 ( 4, 3, 3, 3, 4 ),
 ( -3.224855718271604415E-06, 0.000000000000000000, 6.199515528660412213E-06, 4.034952380126980364E-05, 7.452715123698976899E-05 ),
 .UNSPECIFIED. ) ;
#3781=CARTESIAN_POINT ( 'NONE',  ( -16.89268316805465986, 30.21221237062500720, -234.8082435139909592 ) ) ;
#3875=AXIS2_PLACEMENT_3D ( 'NONE', #112275, #53568, #151402 ) ;
#3939=CARTESIAN_POINT ( 'NONE',  ( -16.81744102076749314, 22.97806745954242302, -230.9350634111226270 ) ) ;
#4000=CARTESIAN_POINT ( 'NONE',  ( -16.94389599338512298, 22.96018495058455855, -230.8787477556889769 ) ) ;
#4056=ORIENTED_EDGE ( 'NONE', *, *, #10821, .F. ) ;
#4069=CARTESIAN_POINT ( 'NONE',  ( 18.54999999999999716, 22.41143600680915426, -231.9928577185252152 ) ) ;
#4210=FACE_OUTER_BOUND ( 'NONE', #202192, .T. ) ;
#4222=EDGE_CURVE ( 'NONE', #245289, #125503, #205470, .T. ) ;
#4259=ORIENTED_EDGE ( 'NONE', *, *, #86054, .F. ) ;
#4271=ORIENTED_EDGE ( 'NONE', *, *, #97443, .T. ) ;
#4306=CARTESIAN_POINT ( 'NONE',  ( -18.36973785203556275, 33.92374417663404529, -235.0677769530471153 ) ) ;
#4398=LINE ( 'NONE', #83900, #111498 ) ;
#4404=EDGE_CURVE ( 'NONE', #46929, #195949, #102184, .T. ) ;
#4464=AXIS2_PLACEMENT_3D ( 'NONE', #195491, #169524, #249035 ) ;
#4604=ADVANCED_FACE ( 'NONE', ( #210325 ), #48229, .F. ) ;
#4651=CARTESIAN_POINT ( 'NONE',  ( -12.92414019175887319, 27.57398452308369485, -234.0009067267211833 ) ) ;
#4686=CARTESIAN_POINT ( 'NONE',  ( 15.57250062127603130, 27.00310224281249205, -233.7483545961832760 ) ) ;
#4776=FACE_OUTER_BOUND ( 'NONE', #15537, .T. ) ;
#4908=DIRECTION ( 'NONE',  ( 1.000000000000000000, 0.000000000000000000, 0.000000000000000000 ) ) ;
#4941=ORIENTED_EDGE ( 'NONE', *, *, #240103, .F. ) ;
#5154=VERTEX_POINT ( 'NONE', #57330 ) ;
#5176=( BOUNDED_SURFACE ( )  B_SPLINE_SURFACE ( 3, 2, ( 
 ( #36770, #154155, #152866 ),
 ( #193246, #251921, #137118 ),
 ( #138371, #133265, #38041 ),
 ( #18451, #176269, #155437 ) ),
 .UNSPECIFIED., .F., .F., .F. ) 
 B_SPLINE_SURFACE_WITH_KNOTS ( ( 4, 4 ),
 ( 3, 3 ),
 ( 0.3000847527772383394, 0.5552748953338751958 ),
 ( 0.000000000000000000, 1.000000000000000000 ),
 .UNSPECIFIED. ) 
 GEOMETRIC_REPRESENTATION_ITEM ( )  RATIONAL_B_SPLINE_SURFACE ( (
 ( 1.000000000000000000, 0.9152888060719235330, 1.000000000000000000),
 ( 1.000000000000000000, 0.9104333467450104189, 1.000000000000000000),
 ( 1.000000000000000000, 0.9035312726220521284, 1.000000000000000000),
 ( 1.000000000000000000, 0.8946697475931482124, 1.000000000000000000) ) ) 
 REPRESENTATION_ITEM ( '' )  SURFACE ( )  );
#5246=VERTEX_POINT ( 'NONE', #42928 ) ;
#5419=EDGE_CURVE ( 'NONE', #69020, #118333, #194968, .T. ) ;
#5602=ORIENTED_EDGE ( 'NONE', *, *, #18960, .T. ) ;
#5656=CARTESIAN_POINT ( 'NONE',  ( -16.81744102076748959, 30.20632856012693424, -234.8070450048000737 ) ) ;
#5734=CARTESIAN_POINT ( 'NONE',  ( 18.54999999999999716, 19.41435213583508812, -230.3874019357809289 ) ) ;
#5931=CARTESIAN_POINT ( 'NONE',  ( -15.75000000000000355, 26.30888228346803004, -233.3999513616626587 ) ) ;
#6139=CARTESIAN_POINT ( 'NONE',  ( -16.91256925476571027, 22.89123816192538996, -230.8480166193616299 ) ) ;
#6177=EDGE_LOOP ( 'NONE', ( #250701, #217880, #50823, #12338, #150763 ) ) ;
#6194=ADVANCED_FACE ( 'NONE', ( #146089 ), #27484, .F. ) ;
#6217=DIRECTION ( 'NONE',  ( -1.020425574104003999E-15, -0.8814952561688429444, 0.4721928772777345684 ) ) ;
#6599=ORIENTED_EDGE ( 'NONE', *, *, #86054, .T. ) ;
#6954=EDGE_CURVE ( 'NONE', #124932, #295, #47319, .T. ) ;
#7058=LINE ( 'NONE', #206552, #199931 ) ;
#7360=CARTESIAN_POINT ( 'NONE',  ( -18.34374000495060386, 20.70020979027691155, -227.9869476361872103 ) ) ;
#7736=ORIENTED_EDGE ( 'NONE', *, *, #143479, .T. ) ;
#7865=EDGE_LOOP ( 'NONE', ( #35168, #113948, #236834, #98657 ) ) ;
#7904=LINE ( 'NONE', #87405, #206527 ) ;
#8058=ORIENTED_EDGE ( 'NONE', *, *, #171497, .T. ) ;
#8114=ORIENTED_EDGE ( 'NONE', *, *, #22855, .T. ) ;
#8195=VECTOR ( 'NONE', #217408, 1000.000000000000114 ) ;
#8230=CARTESIAN_POINT ( 'NONE',  ( 20.73486653747090003, 28.93140779147706709, -237.1870821964558900 ) ) ;
#8266=CARTESIAN_POINT ( 'NONE',  ( -16.93211319090181988, 30.29384521580290013, -234.7972184746587914 ) ) ;
#8394=CARTESIAN_POINT ( 'NONE',  ( 15.39793903038207112, 25.37811339336344929, -232.8563427119264873 ) ) ;
#8651=CARTESIAN_POINT ( 'NONE',  ( -16.93906926870270624, 22.92230643617488539, -230.8346921063524064 ) ) ;
#8763=CARTESIAN_POINT ( 'NONE',  ( -23.25000000000000355, 19.98098358856834977, -229.3296076283783407 ) ) ;
#8805=PLANE ( 'NONE',  #213182 ) ;
#8976=FACE_OUTER_BOUND ( 'NONE', #249700, .T. ) ;
#9149=VERTEX_POINT ( 'NONE', #14089 ) ;
#9294=EDGE_CURVE ( 'NONE', #205806, #219246, #148221, .T. ) ;
#9388=CARTESIAN_POINT ( 'NONE',  ( -16.81930730667008334, 23.03959843057016244, -230.9827737272960917 ) ) ;
#9458=DIRECTION ( 'NONE',  ( -0.000000000000000000, -0.8814952561688430555, 0.4721928772777346239 ) ) ;
#9574=DIRECTION ( 'NONE',  ( -0.000000000000000000, 0.8814952561688430555, -0.4721928772777346239 ) ) ;
#9663=CARTESIAN_POINT ( 'NONE',  ( 13.12220780326571834, 25.00864058361856834, -232.6119739634631287 ) ) ;
#9731=CARTESIAN_POINT ( 'NONE',  ( -14.45443560709635733, 24.86329420051411532, -232.5114740807002534 ) ) ;
#9841=CARTESIAN_POINT ( 'NONE',  ( 13.12229106158773639, 27.68529808098226752, -234.0457819887454320 ) ) ;
#9877=DIRECTION ( 'NONE',  ( -0.000000000000000000, 0.8814952561688430555, -0.4721928772777346239 ) ) ;
#9889=CARTESIAN_POINT ( 'NONE',  ( -18.40000000000000213, 20.94763808724815846, -234.7254930126486556 ) ) ;
#9934=CARTESIAN_POINT ( 'NONE',  ( -16.94062896051973865, 22.95638267382587117, -230.8749853720285898 ) ) ;
#10127=CARTESIAN_POINT ( 'NONE',  ( -16.92973740335347443, 30.27581433217048357, -234.7960487711081043 ) ) ;
#10699=ORIENTED_EDGE ( 'NONE', *, *, #10821, .T. ) ;
#10753=CARTESIAN_POINT ( 'NONE',  ( 15.48841904831874849, 29.55072697483408817, -236.0309298094674944 ) ) ;
#10821=EDGE_CURVE ( 'NONE', #5154, #102599, #191423, .T. ) ;
#10834=CARTESIAN_POINT ( 'NONE',  ( -16.87998658237768623, 30.01800629463564363, -234.7061659226108929 ) ) ;
#11046=CARTESIAN_POINT ( 'NONE',  ( -16.77902162784673834, 22.98694688306329326, -230.9438819989467220 ) ) ;
#11282=VERTEX_POINT ( 'NONE', #77514 ) ;
#11302=CARTESIAN_POINT ( 'NONE',  ( -14.00000000000000178, 26.54497872210690090, -232.9592037335782209 ) ) ;
#11661=CYLINDRICAL_SURFACE ( 'NONE', #118626, 0.09999999999999939493 ) ;
#11752=DIRECTION ( 'NONE',  ( 1.000000000000000000, 0.000000000000000000, 0.000000000000000000 ) ) ;
#11825=B_SPLINE_CURVE_WITH_KNOTS ( 'NONE', 3,
 ( #253895, #76544, #156124, #75301, #31050, #154835, #234334, #110540, #179527, #37448 ),
 .UNSPECIFIED., .F., .F.,
 ( 4, 3, 3, 4 ),
 ( 0.000000000000000000, 4.874959354402468362E-05, 9.785140065121357639E-05, 0.0001360444631936129551 ),
 .UNSPECIFIED. ) ;
#11858=FACE_OUTER_BOUND ( 'NONE', #139824, .T. ) ;
#12088=VERTEX_POINT ( 'NONE', #140423 ) ;
#12140=CARTESIAN_POINT ( 'NONE',  ( -16.77180007708460963, 30.21900964602406248, -234.8138379153629387 ) ) ;
#12257=CARTESIAN_POINT ( 'NONE',  ( 12.60053434924910576, 25.37977472455730776, -232.8574044443169271 ) ) ;
#12300=ORIENTED_EDGE ( 'NONE', *, *, #51111, .F. ) ;
#12336=CARTESIAN_POINT ( 'NONE',  ( -13.54795643572458275, 24.86276468521554506, -232.5111033352153811 ) ) ;
#12338=ORIENTED_EDGE ( 'NONE', *, *, #38942, .F. ) ;
#12435=CARTESIAN_POINT ( 'NONE',  ( 13.77030915526558452, 27.89153536508384335, -234.1274767587460133 ) ) ;
#12527=CARTESIAN_POINT ( 'NONE',  ( -16.94107738177415712, 22.92025126680846725, -230.8312174982872591 ) ) ;
#12799=VECTOR ( 'NONE', #134315, 1000.000000000000000 ) ;
#12984=LINE ( 'NONE', #74251, #199254 ) ;
#13012=ORIENTED_EDGE ( 'NONE', *, *, #16454, .F. ) ;
#13328=FACE_OUTER_BOUND ( 'NONE', #184886, .T. ) ;
#13346=VERTEX_POINT ( 'NONE', #28266 ) ;
#13496=CARTESIAN_POINT ( 'NONE',  ( -21.64999999999999858, 30.16539832223782369, -234.6716761914553899 ) ) ;
#14089=CARTESIAN_POINT ( 'NONE',  ( 18.54999999999999716, 22.97806745954237329, -230.9350634111225986 ) ) ;
#14380=DIRECTION ( 'NONE',  ( 0.000000000000000000, -0.8814952561688430555, 0.4721928772777346239 ) ) ;
#14382=EDGE_CURVE ( 'NONE', #243571, #125503, #220042, .T. ) ;
#14426=DIRECTION ( 'NONE',  ( -1.000000000000000000, 0.000000000000000000, -0.000000000000000000 ) ) ;
#14439=ORIENTED_EDGE ( 'NONE', *, *, #170689, .T. ) ;
#14629=DIRECTION ( 'NONE',  ( -1.000000000000000000, 0.000000000000000000, 0.000000000000000000 ) ) ;
#14711=CARTESIAN_POINT ( 'NONE',  ( -16.79270642812319991, 30.19479984366789438, -234.8051300827147259 ) ) ;
#14739=LINE ( 'NONE', #35588, #249197 ) ;
#14997=CARTESIAN_POINT ( 'NONE',  ( 12.93279065517212700, 27.56753475832528011, -233.9973862756306744 ) ) ;
#15068=CARTESIAN_POINT ( 'NONE',  ( -33.72168855820452649, 33.06517536918362055, -220.7872234046467952 ) ) ;
#15158=CIRCLE ( 'NONE', #148444, 1.749999999999998002 ) ;
#15393=CARTESIAN_POINT ( 'NONE',  ( 20.27550659511089037, 29.85975963366233898, -235.4540239816438429 ) ) ;
#15508=ORIENTED_EDGE ( 'NONE', *, *, #51111, .T. ) ;
#15537=EDGE_LOOP ( 'NONE', ( #95086, #155109, #39859, #108724, #101982, #196386, #60827, #78650, #19642, #1982, #35311, #142590 ) ) ;
#15701=SHAPE_DEFINITION_REPRESENTATION ( #186745, #1804 ) ;
#15750=FACE_OUTER_BOUND ( 'NONE', #44696, .T. ) ;
#15757=LINE ( 'NONE', #22163, #224292 ) ;
#15992=CARTESIAN_POINT ( 'NONE',  ( -16.84981964351505468, 29.99731868204598939, -234.7321595084263492 ) ) ;
#16007=AXIS2_PLACEMENT_3D ( 'NONE', #53217, #132775, #192738 ) ;
#16137=SURFACE_STYLE_FILL_AREA ( #240303 ) ;
#16158=AXIS2_PLACEMENT_3D ( 'NONE', #214349, #192233, #93106 ) ;
#16236=SURFACE_STYLE_USAGE ( .BOTH. , #31948 ) ;
#16331=CARTESIAN_POINT ( 'NONE',  ( -20.65000000000000568, 18.70606281991846842, -231.7096448200342138 ) ) ;
#16454=EDGE_CURVE ( 'NONE', #87552, #12088, #135438, .T. ) ;
#16531=DIRECTION ( 'NONE',  ( 1.000000000000000000, 0.000000000000000000, 0.000000000000000000 ) ) ;
#16686=CARTESIAN_POINT ( 'NONE',  ( -17.01473183483380680, 30.11817903451004952, -234.7598257170722889 ) ) ;
#16714=DIRECTION ( 'NONE',  ( 1.000000000000000000, 0.000000000000000000, 0.000000000000000000 ) ) ;
#17312=LINE ( 'NONE', #118977, #126142 ) ;
#17617=CARTESIAN_POINT ( 'NONE',  ( -16.79363873026997922, 30.20239522323781856, -234.8062423651074653 ) ) ;
#17649=ORIENTED_EDGE ( 'NONE', *, *, #84753, .F. ) ;
#17999=ORIENTED_EDGE ( 'NONE', *, *, #151713, .T. ) ;
#18044=CARTESIAN_POINT ( 'NONE',  ( -21.65000000000000213, 28.93140779147704933, -237.1870821964559184 ) ) ;
#18155=DIRECTION ( 'NONE',  ( 0.7071067811865462405, -0.3338907855510739875, -0.6233112732207629625 ) ) ;
#18193=CARTESIAN_POINT ( 'NONE',  ( 20.73486653747088582, 18.70606281991848974, -231.7096448200341854 ) ) ;
#18218=ORIENTED_EDGE ( 'NONE', *, *, #179507, .T. ) ;
#18361=VERTEX_POINT ( 'NONE', #28150 ) ;
#18432=CARTESIAN_POINT ( 'NONE',  ( -20.65000000000000568, 17.95055421627409231, -233.1200372299043693 ) ) ;
#18451=CARTESIAN_POINT ( 'NONE',  ( -18.44085059012131822, 33.93338217529301204, -235.0292534346912703 ) ) ;
#18514=EDGE_CURVE ( 'NONE', #137205, #171663, #532, .T. ) ;
#18760=ORIENTED_EDGE ( 'NONE', *, *, #173721, .F. ) ;
#18763=ORIENTED_EDGE ( 'NONE', *, *, #218098, .F. ) ;
#18954=EDGE_CURVE ( 'NONE', #26637, #113, #1751, .T. ) ;
#18960=EDGE_CURVE ( 'NONE', #244396, #109775, #216385, .T. ) ;
#19302=CYLINDRICAL_SURFACE ( 'NONE', #222617, 0.1000000000000013933 ) ;
#19402=CARTESIAN_POINT ( 'NONE',  ( -16.94107738177414291, 30.32481141862675145, -234.7976376674202186 ) ) ;
#19440=DIRECTION ( 'NONE',  ( 1.073024830501117528E-15, 0.8814952561688430555, -0.4721928772777346239 ) ) ;
#19485=CARTESIAN_POINT ( 'NONE',  ( -16.95709691156270793, 22.98693315318278252, -230.9398125205108840 ) ) ;
#19492=CARTESIAN_POINT ( 'NONE',  ( -16.93935632781549572, 30.25768881656566123, -234.7951577570964901 ) ) ;
#19538=CARTESIAN_POINT ( 'NONE',  ( -21.65000000000000213, 18.70606281991846842, -231.7096448200342138 ) ) ;
#19642=ORIENTED_EDGE ( 'NONE', *, *, #151180, .F. ) ;
#19655=AXIS2_PLACEMENT_3D ( 'NONE', #206078, #11752, #131671 ) ;
#19684=EDGE_CURVE ( 'NONE', #103509, #100947, #60548, .T. ) ;
#19703=EDGE_LOOP ( 'NONE', ( #199129, #86771, #217954, #94055, #211050 ) ) ;
#19838=CARTESIAN_POINT ( 'NONE',  ( 20.09999999999999787, 22.88362888408688178, -231.1113624623563965 ) ) ;
#20061=CARTESIAN_POINT ( 'NONE',  ( -16.87333278164172867, 23.37215640887969670, -231.2226159629232711 ) ) ;
#20107=VECTOR ( 'NONE', #210053, 1000.000000000000000 ) ;
#20378=ORIENTED_EDGE ( 'NONE', *, *, #188646, .T. ) ;
#20402=DIRECTION ( 'NONE',  ( -1.073024830501117528E-15, -0.8814952561688430555, 0.4721928772777346239 ) ) ;
#20419=VERTEX_POINT ( 'NONE', #67508 ) ;
#20540=MANIFOLD_SOLID_BREP ( 'Stock-MAS-200-1', #94959 ) ;
#20567=DIRECTION ( 'NONE',  ( -1.000000000000000000, 0.000000000000000000, 0.000000000000000000 ) ) ;
#21061=ORIENTED_EDGE ( 'NONE', *, *, #224087, .T. ) ;
#21204=CARTESIAN_POINT ( 'NONE',  ( 16.87683809663749557, 30.20632856012693068, -234.8070450048000737 ) ) ;
#21282=( BOUNDED_SURFACE ( )  B_SPLINE_SURFACE ( 3, 2, ( 
 ( #45284, #6139, #21876 ),
 ( #242191, #23178, #66128 ),
 ( #46546, #180951, #201780 ),
 ( #126084, #106512, #186082 ) ),
 .UNSPECIFIED., .F., .F., .F. ) 
 B_SPLINE_SURFACE_WITH_KNOTS ( ( 4, 4 ),
 ( 3, 3 ),
 ( 0.0008258556059633677133, 0.0009616864997632747171 ),
 ( 0.000000000000000000, 1.000000000000000000 ),
 .UNSPECIFIED. ) 
 GEOMETRIC_REPRESENTATION_ITEM ( )  RATIONAL_B_SPLINE_SURFACE ( (
 ( 1.000000000000000000, 0.9152888060719329699, 1.000000000000000000),
 ( 1.000000000000000000, 0.9327727094137943098, 1.000000000000000000),
 ( 1.000000000000000000, 0.9369023509258086468, 1.000000000000000000),
 ( 1.000000000000000000, 0.9246339933864506921, 1.000000000000000000) ) ) 
 REPRESENTATION_ITEM ( '' )  SURFACE ( )  );
#21291=CARTESIAN_POINT ( 'NONE',  ( -14.00000000000000178, 26.54497872210690090, -232.9592037335782209 ) ) ;
#21630=VECTOR ( 'NONE', #139452, 1000.000000000000000 ) ;
#21680=CARTESIAN_POINT ( 'NONE',  ( -15.06720934482788543, 27.56753475832528011, -233.9973862756307312 ) ) ;
#21876=CARTESIAN_POINT ( 'NONE',  ( -16.87036670365549895, 22.88247411645692253, -230.8391385443351282 ) ) ;
#22025=B_SPLINE_CURVE_WITH_KNOTS ( 'NONE', 3,
 ( #65425, #144947, #2870, #116732, #45864, #178015, #17617, #155891, #224497, #82392 ),
 .UNSPECIFIED., .F., .F.,
 ( 4, 3, 3, 4 ),
 ( -2.000561356211851792E-06, 0.000000000000000000, 1.787822682428855288E-05, 4.206475347089862486E-05 ),
 .UNSPECIFIED. ) ;
#22163=CARTESIAN_POINT ( 'NONE',  ( -21.65000000000000213, 23.06621698515930063, -230.9822826988504119 ) ) ;
#22324=CARTESIAN_POINT ( 'NONE',  ( -20.65000000000000568, 28.17589918783267322, -238.5974746063260739 ) ) ;
#22406=CARTESIAN_POINT ( 'NONE',  ( -16.94107738177415712, 22.92025126680846725, -230.8312174982872591 ) ) ;
#22855=EDGE_CURVE ( 'NONE', #25903, #166513, #190178, .T. ) ;
#23178=CARTESIAN_POINT ( 'NONE',  ( -16.89797118371617302, 22.91357555947262981, -230.8705896228633776 ) ) ;
#23186=EDGE_CURVE ( 'NONE', #5246, #155129, #248600, .T. ) ;
#23374=CARTESIAN_POINT ( 'NONE',  ( -16.87331047859649757, 30.20632856012693424, -234.8070450048000737 ) ) ;
#23501=EDGE_CURVE ( 'NONE', #40232, #124932, #233267, .T. ) ;
#23521=EDGE_LOOP ( 'NONE', ( #8114, #137354, #137297, #166954 ) ) ;
#23592=EDGE_CURVE ( 'NONE', #34034, #244396, #7058, .T. ) ;
#23593=VECTOR ( 'NONE', #234063, 1000.000000000000000 ) ;
#23858=CARTESIAN_POINT ( 'NONE',  ( -16.77683809663752257, 22.98839712131283974, -230.9453208111996503 ) ) ;
#23962=CARTESIAN_POINT ( 'NONE',  ( -16.87331047859651179, 22.97806745954242302, -230.9350634111226270 ) ) ;
#24065=LINE ( 'NONE', #5734, #24583 ) ;
#24094=AXIS2_PLACEMENT_3D ( 'NONE', #49992, #9574, #73440 ) ;
#24260=CARTESIAN_POINT ( 'NONE',  ( -13.77083647240106679, 27.90214353194706476, -234.1315669640961801 ) ) ;
#24284=ORIENTED_EDGE ( 'NONE', *, *, #191991, .T. ) ;
#24295=CARTESIAN_POINT ( 'NONE',  ( 15.73863059295127442, 26.51187484352280421, -233.5070971077067554 ) ) ;
#24583=VECTOR ( 'NONE', #85264, 1000.000000000000000 ) ;
#24880=CARTESIAN_POINT ( 'NONE',  ( -16.91247567987037215, 22.96360194920584163, -230.9170109094160068 ) ) ;
#25223=DIRECTION ( 'NONE',  ( -1.000000000000000000, -0.000000000000000000, -0.000000000000000000 ) ) ;
#25534=CARTESIAN_POINT ( 'NONE',  ( -14.11361717019516249, 27.90226189425600367, -234.1316127586030120 ) ) ;
#25569=CARTESIAN_POINT ( 'NONE',  ( 14.45963434102923983, 27.85878770204270083, -234.1150007431636766 ) ) ;
#25755=ORIENTED_EDGE ( 'NONE', *, *, #212473, .F. ) ;
#25903=VERTEX_POINT ( 'NONE', #233756 ) ;
#25929=DIRECTION ( 'NONE',  ( -0.000000000000000000, 0.8814952561688430555, -0.4721928772777346239 ) ) ;
#26469=CYLINDRICAL_SURFACE ( 'NONE', #41963, 0.09999999999999684142 ) ;
#26489=DIRECTION ( 'NONE',  ( 1.000000000000000000, 5.603460673774840016E-17, 1.046060675573451769E-16 ) ) ;
#26637=VERTEX_POINT ( 'NONE', #590 ) ;
#27046=ORIENTED_EDGE ( 'NONE', *, *, #92523, .F. ) ;
#27484=PLANE ( 'NONE',  #19655 ) ;
#27763=EDGE_CURVE ( 'NONE', #103956, #170251, #140137, .T. ) ;
#28058=ORIENTED_EDGE ( 'NONE', *, *, #50746, .T. ) ;
#28150=CARTESIAN_POINT ( 'NONE',  ( 20.09999999999999787, 30.11188998467138944, -234.9833440560338147 ) ) ;
#28266=CARTESIAN_POINT ( 'NONE',  ( -16.87683809663752399, 29.49590395944699139, -234.5399335999045718 ) ) ;
#28668=ORIENTED_EDGE ( 'NONE', *, *, #246962, .T. ) ;
#28704=VECTOR ( 'NONE', #198170, 1000.000000000000000 ) ;
#29052=ORIENTED_EDGE ( 'NONE', *, *, #251102, .F. ) ;
#29120=DIRECTION ( 'NONE',  ( -1.186688945009009584E-16, 0.4721928772777345684, 0.8814952561688429444 ) ) ;
#29152=CARTESIAN_POINT ( 'NONE',  ( -16.97048361161166952, 29.77341243951207872, -234.5751436903205160 ) ) ;
#29486=CARTESIAN_POINT ( 'NONE',  ( 23.24999999999999645, 19.44861527341281615, -230.3234391047226666 ) ) ;
#30334=LINE ( 'NONE', #31637, #180673 ) ;
#30357=AXIS2_PLACEMENT_3D ( 'NONE', #46358, #43816, #105019 ) ;
#30444=B_SPLINE_CURVE_WITH_KNOTS ( 'NONE', 3,
 ( #87963, #243202, #67146, #247049, #47563, #204076, #85384, #68440, #227492, #108832, #9731, #50138, #74887, #31904, #153149, #12336, #55251, #133540, #253476, #52708, #231372, #150545, #113967, #154430, #72298, #190976 ),
 .UNSPECIFIED., .F., .F.,
 ( 4, 2, 2, 2, 2, 2, 2, 2, 2, 2, 2, 2, 4 ),
 ( 0.005476422646581350848, 0.006160811967703534037, 0.006845201288825718093, 0.007187395949386826167, 0.007529590609947933375, 0.007871785270509041449, 0.008213979931070149523, 0.008556174591631257598, 0.008898369252192365672, 0.009240563912753473746, 0.009582758573314580086, 0.01026714789443682226, 0.01095153721555906443 ),
 .UNSPECIFIED. ) ;
#30535=CARTESIAN_POINT ( 'NONE',  ( 15.74999999999999645, 26.30888228346803714, -233.3999513616626587 ) ) ;
#30538=LINE ( 'NONE', #170076, #178232 ) ;
#30634=CARTESIAN_POINT ( 'NONE',  ( -16.81744102076749314, 22.97806745954242302, -230.9350634111226270 ) ) ;
#30722=CARTESIAN_POINT ( 'NONE',  ( 12.30626653967340900, 26.71301589465422310, -233.6087318245599249 ) ) ;
#30811=CARTESIAN_POINT ( 'NONE',  ( -16.93262454970420094, 22.93468882618020999, -230.8528127703816040 ) ) ;
#30938=EDGE_CURVE ( 'NONE', #173445, #244396, #233315, .T. ) ;
#31050=CARTESIAN_POINT ( 'NONE',  ( -16.86422026484317271, 22.92796883769972283, -230.8850307275119178 ) ) ;
#31152=CARTESIAN_POINT ( 'NONE',  ( 13.99999999999999822, 26.54497872210689735, -232.9592037335782209 ) ) ;
#31393=EDGE_CURVE ( 'NONE', #11282, #133539, #198109, .T. ) ;
#31503=ADVANCED_FACE ( 'NONE', ( #8976 ), #130191, .F. ) ;
#31539=DIRECTION ( 'NONE',  ( -1.000000000000000000, -0.000000000000000000, -0.000000000000000000 ) ) ;
#31637=CARTESIAN_POINT ( 'NONE',  ( 21.72449340488910607, 20.13867536412185189, -229.0352267540020819 ) ) ;
#31867=VERTEX_POINT ( 'NONE', #249544 ) ;
#31887=CYLINDRICAL_SURFACE ( 'NONE', #16158, 1.500000000000001332 ) ;
#31904=CARTESIAN_POINT ( 'NONE',  ( -13.88555196119803803, 24.81692076904266386, -232.4788742220511608 ) ) ;
#31948=SURFACE_SIDE_STYLE ('',( #235249 ) ) ;
#32090=CARTESIAN_POINT ( 'NONE',  ( -16.93772744219066340, 22.95284413564059278, -230.8721573634133222 ) ) ;
#32280=CARTESIAN_POINT ( 'NONE',  ( -16.85718274719385690, 30.29505757199756033, -234.8249179232091137 ) ) ;
#32290=ORIENTED_EDGE ( 'NONE', *, *, #31393, .T. ) ;
#32465=MECHANICAL_DESIGN_GEOMETRIC_PRESENTATION_REPRESENTATION('',(#94955),#132379);
#32530=FACE_OUTER_BOUND ( 'NONE', #71294, .T. ) ;
#32583=CIRCLE ( 'NONE', #16007, 0.09999999999999939493 ) ;
#32759=B_SPLINE_CURVE_WITH_KNOTS ( 'NONE', 3,
 ( #30634, #245810, #47585, #247070, #51421, #170170, #206679, #141883, #11046, #90567, #249666, #71043, #150563 ),
 .UNSPECIFIED., .F., .F.,
 ( 4, 3, 3, 3, 4 ),
 ( 1.080553112431203744E-16, 1.946463881814594965E-05, 3.922356109943912858E-05, 4.215060953238345049E-05, 4.415117091092495043E-05 ),
 .UNSPECIFIED. ) ;
#32891=ORIENTED_EDGE ( 'NONE', *, *, #92069, .F. ) ;
#32902=CARTESIAN_POINT ( 'NONE',  ( -18.40000000000000568, 30.96206749086277554, -233.4839438819913653 ) ) ;
#33009=CARTESIAN_POINT ( 'NONE',  ( -16.90138253750125941, 30.08429674386798069, -234.7416759015230241 ) ) ;
#33011=CARTESIAN_POINT ( 'NONE',  ( -16.83558968593863270, 30.19548159561646372, -234.8012345828538514 ) ) ;
#33113=CARTESIAN_POINT ( 'NONE',  ( 15.74999999999999645, 26.54497872210689735, -232.9592037335782209 ) ) ;
#33129=CARTESIAN_POINT ( 'NONE',  ( 13.22261339317536866, 24.96400212477830749, -232.5813472152648558 ) ) ;
#33152=CARTESIAN_POINT ( 'NONE',  ( -12.25000000000000178, 26.30888228346803714, -233.3999513616626587 ) ) ;
#33243=DIRECTION ( 'NONE',  ( 1.186688945009009584E-16, -0.4721928772777346239, -0.8814952561688430555 ) ) ;
#33389=CARTESIAN_POINT ( 'NONE',  ( -16.93302609847409457, 22.94403737378339869, -230.8638760910858707 ) ) ;
#33534=VECTOR ( 'NONE', #16714, 1000.000000000000000 ) ;
#33584=CARTESIAN_POINT ( 'NONE',  ( -16.87036670365548474, 30.33914847462231279, -234.8334748671511818 ) ) ;
#34034=VERTEX_POINT ( 'NONE', #121027 ) ;
#34164=ORIENTED_EDGE ( 'NONE', *, *, #233295, .T. ) ;
#34237=LINE ( 'NONE', #134564, #252164 ) ;
#34486=B_SPLINE_CURVE_WITH_KNOTS ( 'NONE', 3,
 ( #90903, #175596, #4306, #255046, #104666, #195174, #76468 ),
 .UNSPECIFIED., .F., .F.,
 ( 4, 3, 4 ),
 ( 0.000000000000000000, 3.882884552234317513E-05, 5.798605692158501627E-05 ),
 .UNSPECIFIED. ) ;
#34727=VERTEX_POINT ( 'NONE', #62056 ) ;
#34835=CARTESIAN_POINT ( 'NONE',  ( -16.86733706339143524, 30.26070006106851551, -234.8180300960572708 ) ) ;
#35098=CARTESIAN_POINT ( 'NONE',  ( -16.97683809663752186, 22.93084817181464530, -231.0232129367395260 ) ) ;
#35168=ORIENTED_EDGE ( 'NONE', *, *, #247167, .F. ) ;
#35213=ORIENTED_EDGE ( 'NONE', *, *, #216478, .T. ) ;
#35224=DIRECTION ( 'NONE',  ( -0.000000000000000000, 0.8814952561688430555, -0.4721928772777346239 ) ) ;
#35311=ORIENTED_EDGE ( 'NONE', *, *, #27763, .F. ) ;
#35411=ADVANCED_FACE ( 'NONE', ( #214091 ), #176275, .F. ) ;
#35555=CARTESIAN_POINT ( 'NONE',  ( -16.82055514392420648, 30.18270618454418752, -234.7943911448769256 ) ) ;
#35588=CARTESIAN_POINT ( 'NONE',  ( -18.40000000000000213, 34.05335961020092839, -234.8258093264404636 ) ) ;
#36127=VECTOR ( 'NONE', #87995, 1000.000000000000000 ) ;
#36271=ORIENTED_EDGE ( 'NONE', *, *, #163659, .T. ) ;
#36696=VERTEX_POINT ( 'NONE', #4069 ) ;
#36770=CARTESIAN_POINT ( 'NONE',  ( -16.94107738177414291, 30.32481141862674079, -234.7976376674202186 ) ) ;
#37139=CARTESIAN_POINT ( 'NONE',  ( -17.78043020864321022, 21.36579535192818824, -229.0463459100317323 ) ) ;
#37448=CARTESIAN_POINT ( 'NONE',  ( -16.89268316805466341, 22.97380970494227626, -230.9308293615217451 ) ) ;
#37555=ORIENTED_EDGE ( 'NONE', *, *, #69482, .T. ) ;
#37620=VECTOR ( 'NONE', #244285, 1000.000000000000000 ) ;
#37777=CARTESIAN_POINT ( 'NONE',  ( -16.97092634996494454, 22.98459280967489704, -230.8808285843816464 ) ) ;
#37897=CARTESIAN_POINT ( 'NONE',  ( -18.44085059012131822, 20.72804496316922851, -227.9555157940418439 ) ) ;
#38041=CARTESIAN_POINT ( 'NONE',  ( -17.73285935861300544, 32.75820691008978258, -235.1439690831322480 ) ) ;
#38385=( BOUNDED_CURVE ( )  B_SPLINE_CURVE ( 3, ( #127538, #152262, #226619, #113107 ),
 .UNSPECIFIED., .F., .F. ) 
 B_SPLINE_CURVE_WITH_KNOTS ( ( 4, 4 ),
 ( 0.3000847527772390055, 0.5517402753107889524 ),
 .UNSPECIFIED. ) 
 CURVE ( )  GEOMETRIC_REPRESENTATION_ITEM ( )  RATIONAL_B_SPLINE_CURVE ( ( 1.000000000000000000, 0.9947294176030464508, 0.9947294176030464508, 1.000000000000000000 ) ) 
 REPRESENTATION_ITEM ( '' )  );
#38462=EDGE_CURVE ( 'NONE', #101407, #225681, #50272, .T. ) ;
#38669=DIRECTION ( 'NONE',  ( 1.000000000000000000, 0.000000000000000000, 0.000000000000000000 ) ) ;
#38942=EDGE_CURVE ( 'NONE', #67930, #142779, #63933, .T. ) ;
#39066=CARTESIAN_POINT ( 'NONE',  ( -16.92563707711778420, 30.24240912587386276, -234.8048286477303179 ) ) ;
#39382=DIRECTION ( 'NONE',  ( 0.000000000000000000, -0.8814952561688430555, 0.4721928772777346239 ) ) ;
#39387=DIRECTION ( 'NONE',  ( -0.5932847527679296906, 0.3801118060259206510, 0.7095972217059544063 ) ) ;
#39430=CARTESIAN_POINT ( 'NONE',  ( -16.89268316805465986, 30.21221237062500720, -234.8082435139909592 ) ) ;
#39565=( NAMED_UNIT ( * ) SI_UNIT ( $, .STERADIAN. ) SOLID_ANGLE_UNIT ( ) );
#39643=CARTESIAN_POINT ( 'NONE',  ( -16.96982749440685012, 23.39658237464075796, -231.1592503940484846 ) ) ;
#39712=ORIENTED_EDGE ( 'NONE', *, *, #112093, .T. ) ;
#39859=ORIENTED_EDGE ( 'NONE', *, *, #195676, .F. ) ;
#40232=VERTEX_POINT ( 'NONE', #198524 ) ;
#40363=CARTESIAN_POINT ( 'NONE',  ( -16.91049119928364064, 22.95010608342089498, -230.9200852673934605 ) ) ;
#40379=VECTOR ( 'NONE', #107018, 1000.000000000000000 ) ;
#40680=VECTOR ( 'NONE', #144807, 1000.000000000000000 ) ;
#40752=ORIENTED_EDGE ( 'NONE', *, *, #154120, .T. ) ;
#41427=DIRECTION ( 'NONE',  ( -0.000000000000000000, 0.8814952561688430555, -0.4721928772777346239 ) ) ;
#41670=PRODUCT_CONTEXT ( 'NONE', #78994, 'mechanical' ) ;
#41838=VERTEX_POINT ( 'NONE', #252776 ) ;
#41840=VECTOR ( 'NONE', #157361, 1000.000000000000000 ) ;
#41963=AXIS2_PLACEMENT_3D ( 'NONE', #186828, #46008, #228521 ) ;
#42046=EDGE_CURVE ( 'NONE', #156025, #13346, #174373, .T. ) ;
#42154=PLANE ( 'NONE',  #44574 ) ;
#42169=ORIENTED_EDGE ( 'NONE', *, *, #235174, .T. ) ;
#42185=DIRECTION ( 'NONE',  ( 1.000000000000000000, 0.000000000000000000, 0.000000000000000000 ) ) ;
#42537=VERTEX_POINT ( 'NONE', #228246 ) ;
#42549=DIRECTION ( 'NONE',  ( 1.000000000000000000, 0.000000000000000000, 0.000000000000000000 ) ) ;
#42615=CARTESIAN_POINT ( 'NONE',  ( -16.87683809663752399, 23.59405348476682107, -231.3784738672518415 ) ) ;
#42653=VERTEX_POINT ( 'NONE', #155153 ) ;
#42735=DIRECTION ( 'NONE',  ( 1.073024830501117528E-15, 0.8814952561688430555, -0.4721928772777346239 ) ) ;
#42918=CARTESIAN_POINT ( 'NONE',  ( 20.99999999999999645, 19.88654501311280498, -229.5059066796121101 ) ) ;
#42928=CARTESIAN_POINT ( 'NONE',  ( -16.94445028196808778, 22.96031635112858282, -230.8778361528912058 ) ) ;
#43142=CARTESIAN_POINT ( 'NONE',  ( -16.92132318717937522, 22.96133218596934000, -230.9078683685870317 ) ) ;
#43247=ORIENTED_EDGE ( 'NONE', *, *, #150937, .F. ) ;
#43540=CARTESIAN_POINT ( 'NONE',  ( -16.87372397896795917, 29.73344917972452350, -234.6324668538658500 ) ) ;
#43579=MECHANICAL_DESIGN_GEOMETRIC_PRESENTATION_REPRESENTATION('',(#185229),#214821);
#43807=CARTESIAN_POINT ( 'NONE',  ( -12.25000000000000178, 26.30888228346803714, -233.3999513616626587 ) ) ;
#43816=DIRECTION ( 'NONE',  ( -0.000000000000000000, 0.8814952561688430555, -0.4721928772777346239 ) ) ;
#43981=VECTOR ( 'NONE', #83608, 1000.000000000000000 ) ;
#44160=VECTOR ( 'NONE', #157860, 1000.000000000000000 ) ;
#44235=CARTESIAN_POINT ( 'NONE',  ( 17.23472005113827876, 22.09227994357196678, -230.0545770955219211 ) ) ;
#44421=EDGE_LOOP ( 'NONE', ( #104667, #242224, #191629, #155316 ) ) ;
#44537=EDGE_LOOP ( 'NONE', ( #51468, #82506, #168217, #104552 ) ) ;
#44574=AXIS2_PLACEMENT_3D ( 'NONE', #141239, #219475, #62980 ) ;
#44642=DIRECTION ( 'NONE',  ( -0.8049926720990043805, -0.2801448344544986702, -0.5229776951222359083 ) ) ;
#44696=EDGE_LOOP ( 'NONE', ( #79066, #39712, #74394, #240470 ) ) ;
#44850=CARTESIAN_POINT ( 'NONE',  ( 12.25000000000000000, 26.30888228346803004, -233.3999513616626587 ) ) ;
#44859=FACE_OUTER_BOUND ( 'NONE', #62703, .T. ) ;
#44943=CARTESIAN_POINT ( 'NONE',  ( 12.25000000000000000, 26.30888228346803004, -233.3999513616626587 ) ) ;
#45037=EDGE_CURVE ( 'NONE', #239889, #5246, #197205, .T. ) ;
#45061=PRODUCT ( 'Snap Open Cable Crossbars 8', 'Snap Open Cable Crossbars 8', '', ( #41670 ) ) ;
#45084=CARTESIAN_POINT ( 'NONE',  ( -12.68215100488890279, 27.35084141791446655, -233.9052011656355603 ) ) ;
#45112=CARTESIAN_POINT ( 'NONE',  ( -17.11825945287481332, 30.11817903451004952, -234.7598257170722889 ) ) ;
#45119=CARTESIAN_POINT ( 'NONE',  ( -18.34374000495060386, 20.70020979027691155, -227.9869476361872103 ) ) ;
#45284=CARTESIAN_POINT ( 'NONE',  ( -16.94107738177415712, 22.92025126680846725, -230.8312174982872307 ) ) ;
#45855=AXIS2_PLACEMENT_3D ( 'NONE', #240142, #234021, #55349 ) ;
#45864=CARTESIAN_POINT ( 'NONE',  ( -16.78270389226385007, 30.19733697315739818, -234.8052090562477190 ) ) ;
#46008=DIRECTION ( 'NONE',  ( -0.7071067811865456854, 0.3338907855510743206, 0.6233112732207635176 ) ) ;
#46136=EDGE_CURVE ( 'NONE', #93310, #178218, #205548, .T. ) ;
#46183=CARTESIAN_POINT ( 'NONE',  ( 20.04999999999999716, 29.63969710739366548, -235.8648393122026334 ) ) ;
#46330=CARTESIAN_POINT ( 'NONE',  ( 17.23472005113827166, 31.43009469574038661, -235.0565888300789936 ) ) ;
#46358=CARTESIAN_POINT ( 'NONE',  ( 20.99999999999999645, 19.88654501311280498, -229.5059066796121101 ) ) ;
#46546=CARTESIAN_POINT ( 'NONE',  ( -16.92973740335385102, 22.94872168439534832, -230.8711258231723491 ) ) ;
#46800=DIRECTION ( 'NONE',  ( 1.000000000000000000, 0.000000000000000000, 0.000000000000000000 ) ) ;
#46900=DIRECTION ( 'NONE',  ( -1.000000000000000000, 0.000000000000000000, 0.000000000000000000 ) ) ;
#46929=VERTEX_POINT ( 'NONE', #141425 ) ;
#47219=ORIENTED_EDGE ( 'NONE', *, *, #100621, .T. ) ;
#47319=LINE ( 'NONE', #8230, #148628 ) ;
#47357=CARTESIAN_POINT ( 'NONE',  ( -16.93262454970419384, 30.29883458234789728, -234.7975840541324430 ) ) ;
#47479=VECTOR ( 'NONE', #141551, 1000.000000000000000 ) ;
#47563=CARTESIAN_POINT ( 'NONE',  ( -15.39946565075089602, 25.37977472455730776, -232.8574044443168987 ) ) ;
#47585=CARTESIAN_POINT ( 'NONE',  ( -16.80438519320023616, 22.97861394159803439, -230.9356067475303007 ) ) ;
#47664=CARTESIAN_POINT ( 'NONE',  ( -18.40000000000000213, 20.70659057908908096, -227.9750359040556873 ) ) ;
#48229=( BOUNDED_SURFACE ( )  B_SPLINE_SURFACE ( 3, 2, ( 
 ( #109913, #112509, #152944 ),
 ( #173812, #229879, #189473 ),
 ( #151655, #212885, #73402 ),
 ( #132058, #172524, #175086 ),
 ( #15992, #10834, #194631 ),
 ( #171235, #211604, #51203 ),
 ( #193327, #90350, #254538 ),
 ( #232466, #35555, #33011 ),
 ( #14711, #169950, #55061 ),
 ( #95493, #192055, #12140 ) ),
 .UNSPECIFIED., .F., .F., .T. ) 
 B_SPLINE_SURFACE_WITH_KNOTS ( ( 4, 2, 2, 2, 4 ),
 ( 3, 3 ),
 ( 0.002161241639767243466, 0.002579950749615821798, 0.002789305304540111181, 0.002893982582002256089, 0.002998659859464400564 ),
 ( 0.000000000000000000, 1.000000000000000000 ),
 .UNSPECIFIED. ) 
 GEOMETRIC_REPRESENTATION_ITEM ( )  RATIONAL_B_SPLINE_SURFACE ( (
 ( 1.000000000000000000, 0.7071067811865475727, 1.000000000000000000),
 ( 1.000000000000000000, 0.7632447400659836401, 1.000000000000000000),
 ( 1.000000000000000000, 0.8158073005114181431, 1.000000000000000000),
 ( 1.000000000000000000, 0.8906973462394581764, 1.000000000000000000),
 ( 1.000000000000000000, 0.9149408947801753733, 1.000000000000000000),
 ( 1.000000000000000000, 0.9493368785275054789, 1.000000000000000000),
 ( 1.000000000000000000, 0.9605194247162225363, 1.000000000000000000),
 ( 1.000000000000000000, 0.9803630264775601288, 1.000000000000000000),
 ( 1.000000000000000000, 0.9900844824275457645, 1.000000000000000000),
 ( 1.000000000000000000, 0.9894588281429267385, 1.000000000000000000) ) ) 
 REPRESENTATION_ITEM ( '' )  SURFACE ( )  );
#48466=ADVANCED_FACE ( 'NONE', ( #122901 ), #61631, .F. ) ;
#48520=CARTESIAN_POINT ( 'NONE',  ( -16.87683809663752399, 23.59405348476682107, -231.3784738672518415 ) ) ;
#48654=CARTESIAN_POINT ( 'NONE',  ( -16.93521499325732549, 30.27781715495975945, -234.7945324989871096 ) ) ;
#48962=CARTESIAN_POINT ( 'NONE',  ( 12.68104795156994591, 27.34981073572247823, -233.9047583970293260 ) ) ;
#49103=PLANE ( 'NONE',  #92645 ) ;
#49241=CARTESIAN_POINT ( 'NONE',  ( -16.92570016628983254, 30.23634993850275521, -234.8131561248061701 ) ) ;
#49397=ORIENTED_EDGE ( 'NONE', *, *, #38942, .T. ) ;
#49682=ADVANCED_FACE ( 'NONE', ( #11858 ), #233783, .T. ) ;
#49896=ORIENTED_EDGE ( 'NONE', *, *, #211636, .T. ) ;
#49992=CARTESIAN_POINT ( 'NONE',  ( 23.04999999999999716, 19.44861527341281615, -230.3234391047226666 ) ) ;
#50071=CARTESIAN_POINT ( 'NONE',  ( 15.70340296795548873, 25.90497867185233360, -233.1769111789295721 ) ) ;
#50138=CARTESIAN_POINT ( 'NONE',  ( -14.23072895065542376, 24.82647667088539478, -232.4856315176583905 ) ) ;
#50157=EDGE_CURVE ( 'NONE', #102599, #223523, #79179, .T. ) ;
#50272=LINE ( 'NONE', #29486, #67829 ) ;
#50286=DIRECTION ( 'NONE',  ( 0.000000000000000000, 0.4721928772777346239, 0.8814952561688430555 ) ) ;
#50571=EDGE_CURVE ( 'NONE', #74153, #34034, #22025, .T. ) ;
#50631=CARTESIAN_POINT ( 'NONE',  ( -15.75000000000000355, 26.30888228346803004, -233.3999513616626587 ) ) ;
#50746=EDGE_CURVE ( 'NONE', #42537, #103956, #173571, .T. ) ;
#50806=CARTESIAN_POINT ( 'NONE',  ( -18.34374000495059676, 33.92263863280957281, -235.0698407953532296 ) ) ;
#50823=ORIENTED_EDGE ( 'NONE', *, *, #251366, .F. ) ;
#50943=AXIS2_PLACEMENT_3D ( 'NONE', #21291, #81208, #162074 ) ;
#50965=DIRECTION ( 'NONE',  ( 1.000000000000000000, 0.000000000000000000, 0.000000000000000000 ) ) ;
#50994=VERTEX_POINT ( 'NONE', #226755 ) ;
#51111=EDGE_CURVE ( 'NONE', #136504, #173445, #152390, .T. ) ;
#51136=DIRECTION ( 'NONE',  ( -0.000000000000000000, 0.8814952561688430555, -0.4721928772777346239 ) ) ;
#51162=EDGE_LOOP ( 'NONE', ( #246891, #77595, #144885, #2556 ) ) ;
#51203=CARTESIAN_POINT ( 'NONE',  ( -16.88783316861809070, 30.11618329224522128, -234.7587566525756415 ) ) ;
#51240=CARTESIAN_POINT ( 'NONE',  ( -18.40000000000000213, 33.85569253519368260, -235.0339796035492554 ) ) ;
#51326=CARTESIAN_POINT ( 'NONE',  ( 15.06592377766032165, 25.11330806876552657, -232.6826121690050400 ) ) ;
#51375=ORIENTED_EDGE ( 'NONE', *, *, #143766, .T. ) ;
#51421=CARTESIAN_POINT ( 'NONE',  ( -16.79184697841823848, 22.98113411688375507, -230.9381109511705574 ) ) ;
#51468=ORIENTED_EDGE ( 'NONE', *, *, #31393, .F. ) ;
#51806=ORIENTED_EDGE ( 'NONE', *, *, #112093, .F. ) ;
#51852=LINE ( 'NONE', #213509, #169662 ) ;
#51930=EDGE_CURVE ( 'NONE', #41838, #118431, #211357, .T. ) ;
#51966=DIRECTION ( 'NONE',  ( 1.000000000000000000, 0.000000000000000000, 0.000000000000000000 ) ) ;
#52318=DIRECTION ( 'NONE',  ( -0.000000000000000000, 0.8814952561688430555, -0.4721928772777346239 ) ) ;
#52599=ORIENTED_EDGE ( 'NONE', *, *, #134514, .F. ) ;
#52638=CARTESIAN_POINT ( 'NONE',  ( -16.87331047859651179, 22.97806745954242302, -230.9350634111226270 ) ) ;
#52700=EDGE_CURVE ( 'NONE', #109775, #253844, #136487, .T. ) ;
#52708=CARTESIAN_POINT ( 'NONE',  ( -12.93407622233967658, 25.11330806876552657, -232.6826121690050684 ) ) ;
#52805=CARTESIAN_POINT ( 'NONE',  ( 12.33938619321247465, 26.81104512947605656, -233.6567807927322917 ) ) ;
#53217=CARTESIAN_POINT ( 'NONE',  ( -16.97683809663752186, 23.59405348476697739, -231.3784738672519552 ) ) ;
#53362=CARTESIAN_POINT ( 'NONE',  ( 21.13736287352038445, 29.30757664734318624, -236.4848457208103412 ) ) ;
#53383=FACE_OUTER_BOUND ( 'NONE', #211588, .T. ) ;
#53568=DIRECTION ( 'NONE',  ( 0.7071067811865486830, 0.3338907855510734324, 0.6233112732207604090 ) ) ;
#53571=CARTESIAN_POINT ( 'NONE',  ( -18.40000000000000213, 23.82801463864234037, -229.3483719500187306 ) ) ;
#53698=ORIENTED_EDGE ( 'NONE', *, *, #224087, .F. ) ;
#53798=VECTOR ( 'NONE', #151051, 1000.000000000000000 ) ;
#53800=CARTESIAN_POINT ( 'NONE',  ( -16.81453563122429529, 30.14675705701981556, -234.7874993013237486 ) ) ;
#54522=ORIENTED_EDGE ( 'NONE', *, *, #110334, .F. ) ;
#54538=VECTOR ( 'NONE', #175925, 1000.000000000000000 ) ;
#54675=EDGE_CURVE ( 'NONE', #142779, #239027, #73206, .T. ) ;
#54727=ORIENTED_EDGE ( 'NONE', *, *, #234528, .T. ) ;
#54755=ADVANCED_FACE ( 'NONE', ( #173807 ), #74689, .F. ) ;
#55057=CARTESIAN_POINT ( 'NONE',  ( -16.94132844910801339, 30.26709352238295736, -234.7914533465139755 ) ) ;
#55061=CARTESIAN_POINT ( 'NONE',  ( -16.80891096016327424, 30.22189824094511934, -234.8153852565851878 ) ) ;
#55196=ORIENTED_EDGE ( 'NONE', *, *, #58298, .F. ) ;
#55228=AXIS2_PLACEMENT_3D ( 'NONE', #160029, #238249, #144260 ) ;
#55251=CARTESIAN_POINT ( 'NONE',  ( -13.43673303185029333, 24.89049957252425571, -232.5305204729233424 ) ) ;
#55281=CARTESIAN_POINT ( 'NONE',  ( -16.80070461187903064, 22.97539108935011498, -230.9336297528783746 ) ) ;
#55349=DIRECTION ( 'NONE',  ( -1.000000000000000000, -7.774224845003864090E-15, -1.451301502210102000E-14 ) ) ;
#55491=DIRECTION ( 'NONE',  ( -1.652117596168391109E-15, -0.4721928772777345684, -0.8814952561688429444 ) ) ;
#55563=LINE ( 'NONE', #142816, #47479 ) ;
#56345=CARTESIAN_POINT ( 'NONE',  ( -16.94445028196807002, 30.26380394232451465, -234.7901145182196956 ) ) ;
#56566=CARTESIAN_POINT ( 'NONE',  ( -16.84981964351493744, 23.15621314347246340, -231.0675665507066867 ) ) ;
#56573=( GEOMETRIC_REPRESENTATION_CONTEXT ( 3 ) GLOBAL_UNCERTAINTY_ASSIGNED_CONTEXT ( ( #167788 ) ) GLOBAL_UNIT_ASSIGNED_CONTEXT ( ( #231420, #95726, #211856 ) ) REPRESENTATION_CONTEXT ( 'NONE', 'WORKASPACE' ) );
#56834=VERTEX_POINT ( 'NONE', #53362 ) ;
#57060=DIRECTION ( 'NONE',  ( -0.7071067811865456854, 0.3338907855510742650, 0.6233112732207634066 ) ) ;
#57116=CARTESIAN_POINT ( 'NONE',  ( -23.25000000000000355, 30.16539832223782369, -234.6716761914553899 ) ) ;
#57293=CARTESIAN_POINT ( 'NONE',  ( -17.11825945287482753, 23.02528674727019364, -230.8469138855057281 ) ) ;
#57330=CARTESIAN_POINT ( 'NONE',  ( 18.39999999999998082, 20.70020979027691510, -227.9869476361872103 ) ) ;
#57398=DIRECTION ( 'NONE',  ( -1.020425574104003999E-15, 0.8814952561688430555, -0.4721928772777346239 ) ) ;
#57488=VECTOR ( 'NONE', #240189, 1000.000000000000000 ) ;
#57781=FILL_AREA_STYLE_COLOUR ( '', #257224 ) ;
#57814=EDGE_CURVE ( 'NONE', #231239, #100947, #141272, .T. ) ;
#57868=LINE ( 'NONE', #464, #196803 ) ;
#58298=EDGE_CURVE ( 'NONE', #67930, #123629, #7904, .T. ) ;
#59019=ADVANCED_FACE ( 'NONE', ( #166040 ), #126892, .F. ) ;
#59132=CARTESIAN_POINT ( 'NONE',  ( -16.93710578446436088, 23.21501689610121844, -231.0619907376567710 ) ) ;
#59164=ADVANCED_FACE ( 'NONE', ( #238834 ), #61482, .T. ) ;
#59210=VECTOR ( 'NONE', #75492, 999.9999999999998863 ) ;
#59330=CYLINDRICAL_SURFACE ( 'NONE', #72217, 1.749999999999998002 ) ;
#59457=CARTESIAN_POINT ( 'NONE',  ( -16.86379686415369150, 30.29174399807271456, -234.8241917813125781 ) ) ;
#59477=AXIS2_PLACEMENT_3D ( 'NONE', #69725, #86668, #168854 ) ;
#59707=DIRECTION ( 'NONE',  ( 0.000000000000000000, 0.4721928772777346239, 0.8814952561688430555 ) ) ;
#59832=DIRECTION ( 'NONE',  ( -1.000000000000000000, -8.720091142841976186E-15, -1.400634033999624291E-14 ) ) ;
#59951=CARTESIAN_POINT ( 'NONE',  ( -21.64999999999999858, 22.69475173317577443, -231.4639605648239353 ) ) ;
#60049=CARTESIAN_POINT ( 'NONE',  ( 20.73486653747088582, 21.70314669089255943, -233.3151006027784717 ) ) ;
#60260=CARTESIAN_POINT ( 'NONE',  ( -17.11825945287482753, 23.02528674727019364, -230.8469138855057281 ) ) ;
#60548=LINE ( 'NONE', #568, #125414 ) ;
#60665=VERTEX_POINT ( 'NONE', #76309 ) ;
#60781=CARTESIAN_POINT ( 'NONE',  ( -13.11924609551136278, 27.69551741609592810, -234.0500622709108143 ) ) ;
#60827=ORIENTED_EDGE ( 'NONE', *, *, #61764, .T. ) ;
#60951=CARTESIAN_POINT ( 'NONE',  ( -15.55912972643741199, 22.20092727007757460, -232.1740600553843876 ) ) ;
#60975=FACE_OUTER_BOUND ( 'NONE', #78911, .T. ) ;
#61251=DIRECTION ( 'NONE',  ( 1.000000000000000000, 0.000000000000000000, 0.000000000000000000 ) ) ;
#61252=ORIENTED_EDGE ( 'NONE', *, *, #169622, .F. ) ;
#61482=PLANE ( 'NONE',  #183354 ) ;
#61631=PLANE ( 'NONE',  #255939 ) ;
#61663=ADVANCED_FACE ( 'NONE', ( #80483 ), #239608, .F. ) ;
#61764=EDGE_CURVE ( 'NONE', #103509, #12088, #86915, .T. ) ;
#61817=ADVANCED_FACE ( 'NONE', ( #235421 ), #59330, .F. ) ;
#62056=CARTESIAN_POINT ( 'NONE',  ( 22.88900146558018989, 22.38967017749599364, -232.0334904264913973 ) ) ;
#62175=ORIENTED_EDGE ( 'NONE', *, *, #73337, .F. ) ;
#62308=UNCERTAINTY_MEASURE_WITH_UNIT (LENGTH_MEASURE( 1.000000000000000082E-05 ), #137322, 'distance_accuracy_value', 'NONE');
#62352=ORIENTED_EDGE ( 'NONE', *, *, #77474, .T. ) ;
#62469=EDGE_CURVE ( 'NONE', #9149, #223523, #239001, .T. ) ;
#62488=FACE_OUTER_BOUND ( 'NONE', #136159, .T. ) ;
#62703=EDGE_LOOP ( 'NONE', ( #232554, #21061, #152402, #71679 ) ) ;
#62728=CARTESIAN_POINT ( 'NONE',  ( 18.39999999999999503, 33.92263863280957992, -235.0698407953532012 ) ) ;
#62980=DIRECTION ( 'NONE',  ( 0.000000000000000000, 0.8814952561688429444, -0.4721928772777345684 ) ) ;
#63357=FACE_OUTER_BOUND ( 'NONE', #257888, .T. ) ;
#63381=CARTESIAN_POINT ( 'NONE',  ( -18.35663730107557257, 20.70056182099758857, -227.9862904610682222 ) ) ;
#63506=DIRECTION ( 'NONE',  ( 0.000000000000000000, 0.8814952561688430555, -0.4721928772777346239 ) ) ;
#63783=CARTESIAN_POINT ( 'NONE',  ( 18.39999999999998082, 20.70020979027691510, -227.9869476361872103 ) ) ;
#63933=( BOUNDED_CURVE ( )  B_SPLINE_CURVE ( 3, ( #51240, #193368, #195939, #74730 ),
 .UNSPECIFIED., .F., .T. ) 
 B_SPLINE_CURVE_WITH_KNOTS ( ( 4, 4 ),
 ( 5.733388419619901200, 5.983100554402347449 ),
 .UNSPECIFIED. ) 
 CURVE ( )  GEOMETRIC_REPRESENTATION_ITEM ( )  RATIONAL_B_SPLINE_CURVE ( ( 1.000000000000000000, 0.9948104011409417691, 0.9948104011409417691, 1.000000000000000000 ) ) 
 REPRESENTATION_ITEM ( '' )  );
#64270=AXIS2_PLACEMENT_3D ( 'NONE', #166190, #164876, #107461 ) ;
#64292=ORIENTED_EDGE ( 'NONE', *, *, #166988, .F. ) ;
#64427=COLOUR_RGB ( '', 0.31764706, 0.68627451, 0.89019608) ;
#64701=ORIENTED_EDGE ( 'NONE', *, *, #180233, .F. ) ;
#64744=CARTESIAN_POINT ( 'NONE',  ( -16.97683809663753252, 23.52593859471641125, -231.2285429799402721 ) ) ;
#64957=CARTESIAN_POINT ( 'NONE',  ( -17.22361732159832926, 22.03703477488457807, -229.9826991372272573 ) ) ;
#65047=EDGE_CURVE ( 'NONE', #18361, #31867, #123173, .T. ) ;
#65425=CARTESIAN_POINT ( 'NONE',  ( -16.77683809663752257, 30.19206623356022234, -234.8041291499450551 ) ) ;
#65566=CIRCLE ( 'NONE', #98848, 1.500000000000001332 ) ;
#65740=EDGE_LOOP ( 'NONE', ( #116859, #10699, #7736, #95573 ) ) ;
#65873=B_SPLINE_CURVE_WITH_KNOTS ( 'NONE', 3,
 ( #172443, #234949, #215368, #175019 ),
 .UNSPECIFIED., .F., .F.,
 ( 4, 4 ),
 ( 0.000000000000000000, 7.713889350927083648E-05 ),
 .UNSPECIFIED. ) ;
#66128=CARTESIAN_POINT ( 'NONE',  ( -16.85718274719361176, 22.91402687719062570, -230.8711018400638864 ) ) ;
#66211=DIRECTION ( 'NONE',  ( -0.7071067811865486830, 0.3338907855510734324, 0.6233112732207604090 ) ) ;
#66553=CARTESIAN_POINT ( 'NONE',  ( -16.90257928357875628, 22.96791734292147069, -230.9249673455850598 ) ) ;
#66629=ORIENTED_EDGE ( 'NONE', *, *, #38462, .T. ) ;
#66643=VECTOR ( 'NONE', #39387, 1000.000000000000227 ) ;
#66938=CARTESIAN_POINT ( 'NONE',  ( -16.93433913041102912, 30.30801039134145825, -234.7980092385606383 ) ) ;
#67146=CARTESIAN_POINT ( 'NONE',  ( -15.70407651835961360, 25.90710817316711001, -233.1781447626815122 ) ) ;
#67264=CARTESIAN_POINT ( 'NONE',  ( -16.94052228080552069, 30.25905040575426952, -234.7941296169553311 ) ) ;
#67338=CARTESIAN_POINT ( 'NONE',  ( -16.93658211146646408, 22.95103440912690118, -230.8705440892085505 ) ) ;
#67346=AXIS2_PLACEMENT_3D ( 'NONE', #166553, #123546, #165236 ) ;
#67508=CARTESIAN_POINT ( 'NONE',  ( -17.11825945287482753, 23.06621698515930063, -230.9822826988504119 ) ) ;
#67829=VECTOR ( 'NONE', #9877, 1000.000000000000000 ) ;
#67930=VERTEX_POINT ( 'NONE', #78577 ) ;
#68229=CARTESIAN_POINT ( 'NONE',  ( -16.93234230245722216, 30.28871318002137514, -234.7966014547397720 ) ) ;
#68309=ORIENTED_EDGE ( 'NONE', *, *, #45037, .T. ) ;
#68362=CARTESIAN_POINT ( 'NONE',  ( 12.93225390519044815, 25.11447974268060079, -232.6833957968051720 ) ) ;
#68440=CARTESIAN_POINT ( 'NONE',  ( -14.87779219673428877, 25.00864058361856479, -232.6119739634630150 ) ) ;
#68487=LINE ( 'NONE', #209267, #90712 ) ;
#68528=ADVANCED_FACE ( 'NONE', ( #230639 ), #74154, .F. ) ;
#68757=CARTESIAN_POINT ( 'NONE',  ( -12.25000000000000178, 26.54497872210690090, -232.9592037335782209 ) ) ;
#68769=CARTESIAN_POINT ( 'NONE',  ( -14.00000000000000178, 26.54497872210690090, -232.9592037335782209 ) ) ;
#68778=FACE_OUTER_BOUND ( 'NONE', #252782, .T. ) ;
#69020=VERTEX_POINT ( 'NONE', #111649 ) ;
#69174=AXIS2_PLACEMENT_3D ( 'NONE', #183216, #141506, #138901 ) ;
#69190=CARTESIAN_POINT ( 'NONE',  ( -18.40000000000000213, 20.70659057908908096, -227.9750359040556873 ) ) ;
#69198=CARTESIAN_POINT ( 'NONE',  ( -16.97683809663752186, 29.54312324717475136, -234.4517840742877013 ) ) ;
#69438=CARTESIAN_POINT ( 'NONE',  ( -16.87036670365548474, 30.33914847462231279, -234.8334748671511818 ) ) ;
#69442=EDGE_LOOP ( 'NONE', ( #166974, #207652, #147713, #168572 ) ) ;
#69482=EDGE_CURVE ( 'NONE', #89147, #124932, #139558, .T. ) ;
#69510=CARTESIAN_POINT ( 'NONE',  ( -16.77683809663752257, 30.19206623356022234, -234.8041291499450551 ) ) ;
#69664=CARTESIAN_POINT ( 'NONE',  ( -16.87487986503753845, 22.97804876015371889, -230.9350448236104967 ) ) ;
#69725=CARTESIAN_POINT ( 'NONE',  ( 18.54999999999999716, 33.06517536918362055, -220.7872234046467952 ) ) ;
#70592=ORIENTED_EDGE ( 'NONE', *, *, #65047, .F. ) ;
#70624=CARTESIAN_POINT ( 'NONE',  ( -16.87036670365548474, 30.35820049718185487, -234.7353065400981507 ) ) ;
#70960=CARTESIAN_POINT ( 'NONE',  ( 14.77516762759921143, 24.96309550270879285, -232.5807238286745928 ) ) ;
#71043=CARTESIAN_POINT ( 'NONE',  ( -16.77732147278574715, 22.98807097893278595, -230.9449972797045803 ) ) ;
#71049=VECTOR ( 'NONE', #2814, 1000.000000000000000 ) ;
#71146=EDGE_CURVE ( 'NONE', #133539, #11282, #15158, .T. ) ;
#71210=CARTESIAN_POINT ( 'NONE',  ( -16.93583594267724379, 22.92587748271144221, -230.8406021309349399 ) ) ;
#71294=EDGE_LOOP ( 'NONE', ( #232753, #185975, #245934, #192593 ) ) ;
#71474=AXIS2_PLACEMENT_3D ( 'NONE', #171984, #169416, #111982 ) ;
#71660=ORIENTED_EDGE ( 'NONE', *, *, #171973, .F. ) ;
#71679=ORIENTED_EDGE ( 'NONE', *, *, #223798, .T. ) ;
#71844=ADVANCED_FACE ( 'NONE', ( #205035 ), #42154, .F. ) ;
#71945=ORIENTED_EDGE ( 'NONE', *, *, #151220, .T. ) ;
#71948=ORIENTED_EDGE ( 'NONE', *, *, #4404, .F. ) ;
#72029=AXIS2_PLACEMENT_3D ( 'NONE', #60951, #140481, #187343 ) ;
#72161=CARTESIAN_POINT ( 'NONE',  ( 18.39999999999997371, 33.92263863280957281, -235.0698407953532296 ) ) ;
#72167=VECTOR ( 'NONE', #9458, 1000.000000000000000 ) ;
#72217=AXIS2_PLACEMENT_3D ( 'NONE', #214580, #136305, #193748 ) ;
#72225=( BOUNDED_SURFACE ( )  B_SPLINE_SURFACE ( 3, 2, ( 
 ( #33584, #250015, #191357 ),
 ( #32280, #246168, #212188 ),
 ( #109206, #227886, #10127 ),
 ( #251284, #49241, #89642 ) ),
 .UNSPECIFIED., .F., .F., .F. ) 
 B_SPLINE_SURFACE_WITH_KNOTS ( ( 4, 4 ),
 ( 3, 3 ),
 ( 0.0008258556059633741101, 0.0009616864997632823065 ),
 ( 0.000000000000000000, 1.000000000000000000 ),
 .UNSPECIFIED. ) 
 GEOMETRIC_REPRESENTATION_ITEM ( )  RATIONAL_B_SPLINE_SURFACE ( (
 ( 1.000000000000000000, 0.9152888060719235330, 1.000000000000000000),
 ( 1.000000000000000000, 0.9327727094137976405, 1.000000000000000000),
 ( 1.000000000000000000, 0.9369023509258225246, 1.000000000000000000),
 ( 1.000000000000000000, 0.9246339933864551330, 1.000000000000000000) ) ) 
 REPRESENTATION_ITEM ( '' )  SURFACE ( )  );
#72231=CARTESIAN_POINT ( 'NONE',  ( -16.87435696428308063, 22.97806136355487183, -230.9350573516298368 ) ) ;
#72269=EDGE_LOOP ( 'NONE', ( #243177, #32290 ) ) ;
#72295=ORIENTED_EDGE ( 'NONE', *, *, #30938, .F. ) ;
#72298=CARTESIAN_POINT ( 'NONE',  ( -12.24999999999999822, 26.10487691728824799, -233.2906712717671951 ) ) ;
#72495=CARTESIAN_POINT ( 'NONE',  ( -16.93909480342659890, 22.95463988730850957, -230.8736442518436434 ) ) ;
#72790=ORIENTED_EDGE ( 'NONE', *, *, #151220, .F. ) ;
#72899=VECTOR ( 'NONE', #41427, 1000.000000000000000 ) ;
#72942=ADVANCED_FACE ( 'NONE', ( #138669 ), #119516, .F. ) ;
#73083=PLANE ( 'NONE',  #124652 ) ;
#73206=B_SPLINE_CURVE_WITH_KNOTS ( 'NONE', 3,
 ( #166076, #186917, #245589, #66938, #146459, #225977, #47357, #8266, #68229, #147774, #227293, #48654, #251994, #197148, #55057, #56345 ),
 .UNSPECIFIED., .F., .F.,
 ( 4, 3, 3, 3, 3, 4 ),
 ( 0.000000000000000000, 1.810570668010637698E-05, 2.740575833571996995E-05, 4.256816319435940987E-05, 5.213463471026038941E-05, 6.641585710717883072E-05 ),
 .UNSPECIFIED. ) ;
#73337=EDGE_CURVE ( 'NONE', #81187, #100947, #104388, .T. ) ;
#73368=EDGE_CURVE ( 'NONE', #89147, #36696, #65566, .T. ) ;
#73402=CARTESIAN_POINT ( 'NONE',  ( -16.96982749440706328, 29.78781364502790652, -234.5828580218738750 ) ) ;
#73440=DIRECTION ( 'NONE',  ( -1.000000000000000000, 0.000000000000000000, 0.000000000000000000 ) ) ;
#73524=CARTESIAN_POINT ( 'NONE',  ( 15.52844286134408769, 25.54333932933833751, -232.9607505220590440 ) ) ;
#74095=EDGE_CURVE ( 'NONE', #118431, #20419, #117964, .T. ) ;
#74153=VERTEX_POINT ( 'NONE', #69510 ) ;
#74154=PLANE ( 'NONE',  #211556 ) ;
#74240=ORIENTED_EDGE ( 'NONE', *, *, #57814, .F. ) ;
#74251=CARTESIAN_POINT ( 'NONE',  ( 18.39999999999999503, 28.17589918783267322, -238.5974746063260739 ) ) ;
#74394=ORIENTED_EDGE ( 'NONE', *, *, #218098, .T. ) ;
#74447=DIRECTION ( 'NONE',  ( 0.8049926720990052686, 0.2801448344544982261, 0.5229776951222349091 ) ) ;
#74541=DIRECTION ( 'NONE',  ( 1.000000000000000000, 5.603460673774840016E-17, 1.046060675573451769E-16 ) ) ;
#74568=AXIS2_PLACEMENT_3D ( 'NONE', #222017, #143781, #78664 ) ;
#74608=ORIENTED_EDGE ( 'NONE', *, *, #110334, .T. ) ;
#74615=FACE_OUTER_BOUND ( 'NONE', #6177, .T. ) ;
#74689=PLANE ( 'NONE',  #230384 ) ;
#74730=CARTESIAN_POINT ( 'NONE',  ( -16.94107738177414291, 30.32481141862675145, -234.7976376674202186 ) ) ;
#74864=AXIS2_PLACEMENT_3D ( 'NONE', #86794, #205467, #124669 ) ;
#74887=CARTESIAN_POINT ( 'NONE',  ( -14.11697426661281085, 24.81705829073095160, -232.4789712399791028 ) ) ;
#74915=CARTESIAN_POINT ( 'NONE',  ( -16.80621392010911208, 23.00928570187805633, -230.9606318461273702 ) ) ;
#75042=FACE_OUTER_BOUND ( 'NONE', #93205, .T. ) ;
#75301=CARTESIAN_POINT ( 'NONE',  ( -16.86379686415369861, 22.91646731419714200, -230.8734579643043219 ) ) ;
#75321=ADVANCED_FACE ( 'NONE', ( #244751 ), #21282, .T. ) ;
#75492=DIRECTION ( 'NONE',  ( -0.7071067811865462405, 0.3338907855510739875, 0.6233112732207629625 ) ) ;
#75584=CARTESIAN_POINT ( 'NONE',  ( 20.99999999999999645, 30.11188998467138234, -234.9833440560338147 ) ) ;
#75677=CARTESIAN_POINT ( 'NONE',  ( -16.91049119928362998, 30.23428993624846584, -234.8220231485292118 ) ) ;
#75679=CARTESIAN_POINT ( 'NONE',  ( 20.27550659511088682, 22.63149853307782422, -231.5820423879664247 ) ) ;
#75704=DIRECTION ( 'NONE',  ( -0.5932847527679296906, 0.3801118060259212061, 0.7095972217059539622 ) ) ;
#75729=CARTESIAN_POINT ( 'NONE',  ( -17.73285935860374352, 21.28367419047321718, -228.9973760273217920 ) ) ;
#76154=CARTESIAN_POINT ( 'NONE',  ( -16.87683809663748846, 23.64127277249475156, -231.2903243416350563 ) ) ;
#76309=CARTESIAN_POINT ( 'NONE',  ( -23.25000000000000355, 31.05627573922685514, -233.2203535436961488 ) ) ;
#76446=CARTESIAN_POINT ( 'NONE',  ( -18.40000000000000213, 31.05627573922685514, -233.2203535436961488 ) ) ;
#76464=VECTOR ( 'NONE', #82838, 1000.000000000000000 ) ;
#76468=CARTESIAN_POINT ( 'NONE',  ( -18.40000000000000213, 33.92901942162173157, -235.0579290632217067 ) ) ;
#76544=CARTESIAN_POINT ( 'NONE',  ( -16.86578989773641979, 22.89342784614964543, -230.8502347937079264 ) ) ;
#76879=CARTESIAN_POINT ( 'NONE',  ( 23.04999999999999716, 32.67104411594546320, -237.4063322638886859 ) ) ;
#76921=LINE ( 'NONE', #151354, #12799 ) ;
#77119=FACE_OUTER_BOUND ( 'NONE', #208311, .T. ) ;
#77232=LINE ( 'NONE', #215466, #57488 ) ;
#77343=ADVANCED_FACE ( 'NONE', ( #53383 ), #115931, .T. ) ;
#77371=ORIENTED_EDGE ( 'NONE', *, *, #57814, .T. ) ;
#77425=CARTESIAN_POINT ( 'NONE',  ( -16.89155683853296352, 23.53109276876853428, -231.2313039298783508 ) ) ;
#77474=EDGE_CURVE ( 'NONE', #118431, #219246, #177214, .T. ) ;
#77514=CARTESIAN_POINT ( 'NONE',  ( 12.25000000000000000, 26.54497872210689735, -232.9592037335782209 ) ) ;
#77595=ORIENTED_EDGE ( 'NONE', *, *, #23186, .F. ) ;
#78146=CARTESIAN_POINT ( 'NONE',  ( -17.11825945287482753, 22.97806745954241592, -230.9350634111226270 ) ) ;
#78169=PLANE ( 'NONE',  #210515 ) ;
#78260=CARTESIAN_POINT ( 'NONE',  ( 12.25000000000000000, 26.54497872210689735, -232.9592037335782209 ) ) ;
#78577=CARTESIAN_POINT ( 'NONE',  ( -18.40000000000000213, 33.85569253519368260, -235.0339796035492554 ) ) ;
#78650=ORIENTED_EDGE ( 'NONE', *, *, #128636, .F. ) ;
#78654=ORIENTED_EDGE ( 'NONE', *, *, #65047, .T. ) ;
#78664=DIRECTION ( 'NONE',  ( 1.000000000000000000, 0.000000000000000000, 0.000000000000000000 ) ) ;
#78696=ORIENTED_EDGE ( 'NONE', *, *, #115041, .T. ) ;
#78713=CARTESIAN_POINT ( 'NONE',  ( -16.82542659449979894, 23.05416925116509930, -230.9934129395686568 ) ) ;
#78826=ORIENTED_EDGE ( 'NONE', *, *, #92104, .F. ) ;
#78911=EDGE_LOOP ( 'NONE', ( #195311, #211025, #66629, #135549 ) ) ;
#78994=APPLICATION_CONTEXT ( 'automotive_design' ) ;
#79066=ORIENTED_EDGE ( 'NONE', *, *, #185409, .F. ) ;
#79179=LINE ( 'NONE', #256488, #8195 ) ;
#79433=CARTESIAN_POINT ( 'NONE',  ( -16.94389599337536012, 30.26311786373704038, -234.7907289951723158 ) ) ;
#79451=DIRECTION ( 'NONE',  ( -1.073024830501118120E-15, -0.8814952561688430555, 0.4721928772777346239 ) ) ;
#79485=CARTESIAN_POINT ( 'NONE',  ( 20.99999999999999645, 22.88362888408687468, -231.1113624623564249 ) ) ;
#79543=CARTESIAN_POINT ( 'NONE',  ( -17.80356949363709163, 21.33262576353195072, -229.0023278304047949 ) ) ;
#79580=DIRECTION ( 'NONE',  ( -0.000000000000000000, 0.8814952561688430555, -0.4721928772777346239 ) ) ;
#79986=CARTESIAN_POINT ( 'NONE',  ( -16.77308656112215246, 22.97823775711153615, -230.9351546348684110 ) ) ;
#80483=FACE_OUTER_BOUND ( 'NONE', #179750, .T. ) ;
#80511=PLANE ( 'NONE',  #131415 ) ;
#80736=EDGE_CURVE ( 'NONE', #36696, #9149, #236334, .T. ) ;
#81187=VERTEX_POINT ( 'NONE', #102912 ) ;
#81208=DIRECTION ( 'NONE',  ( 1.186688945009009584E-16, -0.4721928772777346239, -0.8814952561688430555 ) ) ;
#81370=( BOUNDED_CURVE ( )  B_SPLINE_CURVE ( 3, ( #63783, #143313, #44235, #217698 ),
 .UNSPECIFIED., .F., .F. ) 
 B_SPLINE_CURVE_WITH_KNOTS ( ( 4, 4 ),
 ( 2.589852378279005940, 2.850972632318389710 ),
 .UNSPECIFIED. ) 
 CURVE ( )  GEOMETRIC_REPRESENTATION_ITEM ( )  RATIONAL_B_SPLINE_CURVE ( ( 1.000000000000000000, 0.9943260843901262636, 0.9943260843901262636, 1.000000000000000000 ) ) 
 REPRESENTATION_ITEM ( '' )  );
#81390=VECTOR ( 'NONE', #221037, 1000.000000000000000 ) ;
#81404=VECTOR ( 'NONE', #42185, 1000.000000000000000 ) ;
#81702=CARTESIAN_POINT ( 'NONE',  ( -16.81744102076749314, 22.97806745954242302, -230.9350634111226270 ) ) ;
#81994=CARTESIAN_POINT ( 'NONE',  ( -16.89081410710458542, 30.21083495796404250, -234.8079631709592832 ) ) ;
#82084=DIRECTION ( 'NONE',  ( -1.000000000000000000, 0.000000000000000000, 0.000000000000000000 ) ) ;
#82208=ORIENTED_EDGE ( 'NONE', *, *, #69482, .F. ) ;
#82297=CARTESIAN_POINT ( 'NONE',  ( -16.77683809663752257, 22.98839712131283974, -230.9453208111996503 ) ) ;
#82341=ORIENTED_EDGE ( 'NONE', *, *, #233295, .F. ) ;
#82370=LINE ( 'NONE', #161965, #111857 ) ;
#82392=CARTESIAN_POINT ( 'NONE',  ( -16.81744102076748959, 30.20632856012693424, -234.8070450048000737 ) ) ;
#82506=ORIENTED_EDGE ( 'NONE', *, *, #189190, .T. ) ;
#82602=ORIENTED_EDGE ( 'NONE', *, *, #104116, .F. ) ;
#82650=CARTESIAN_POINT ( 'NONE',  ( -16.88460203013674388, 30.22258428227766558, -234.8103539652946665 ) ) ;
#82706=ADVANCED_FACE ( 'NONE', ( #198223 ), #207876, .T. ) ;
#82838=DIRECTION ( 'NONE',  ( 1.000000000000000000, 0.000000000000000000, 0.000000000000000000 ) ) ;
#83608=DIRECTION ( 'NONE',  ( 1.652117596168391306E-15, 0.4721928772777346239, 0.8814952561688430555 ) ) ;
#83728=ADVANCED_FACE ( 'NONE', ( #4210 ), #203714, .T. ) ;
#83900=CARTESIAN_POINT ( 'NONE',  ( 20.27550659511089037, 29.85975963366233543, -235.4540239816438429 ) ) ;
#84120=VERTEX_POINT ( 'NONE', #209834 ) ;
#84180=CARTESIAN_POINT ( 'NONE',  ( 15.51872946208854565, 27.09445758862755582, -233.7906081272070651 ) ) ;
#84236=EDGE_CURVE ( 'NONE', #117799, #60665, #196664, .T. ) ;
#84252=CARTESIAN_POINT ( 'NONE',  ( -16.89020380669787968, 23.07274987706156111, -230.9857821902007231 ) ) ;
#84293=ORIENTED_EDGE ( 'NONE', *, *, #255652, .T. ) ;
#84547=CARTESIAN_POINT ( 'NONE',  ( -16.89208623190940273, 30.21172107852033406, -234.8081435470708982 ) ) ;
#84753=EDGE_CURVE ( 'NONE', #146247, #156025, #109493, .T. ) ;
#84825=ORIENTED_EDGE ( 'NONE', *, *, #161191, .T. ) ;
#85016=ORIENTED_EDGE ( 'NONE', *, *, #159478, .T. ) ;
#85139=B_SPLINE_CURVE_WITH_KNOTS ( 'NONE', 3,
 ( #181760, #3094, #43540, #123077, #164766, #172519, #109905, #231180, #53800, #132054, #188184, #211600, #92911, #210318 ),
 .UNSPECIFIED., .F., .F.,
 ( 4, 2, 2, 2, 2, 2, 4 ),
 ( 1.040834085586084257E-17, 0.0003823333598417850043, 0.0005735000397626870746, 0.0006690833797231381368, 0.0007168750497033463207, 0.0007407708846934460759, 0.0007646667196835457226 ),
 .UNSPECIFIED. ) ;
#85264=DIRECTION ( 'NONE',  ( -0.000000000000000000, 0.8814952561688430555, -0.4721928772777346239 ) ) ;
#85349=ADVANCED_FACE ( 'NONE', ( #4776 ), #105291, .F. ) ;
#85384=CARTESIAN_POINT ( 'NONE',  ( -15.06774609480955540, 25.11447974268060435, -232.6833957968052005 ) ) ;
#85392=ADVANCED_FACE ( 'NONE', ( #68778 ), #8805, .F. ) ;
#85455=CARTESIAN_POINT ( 'NONE',  ( -15.51798037960204724, 27.09559348180860283, -233.7911270184622197 ) ) ;
#85486=CARTESIAN_POINT ( 'NONE',  ( 13.88638282980483751, 27.90226189425599657, -234.1316127586029836 ) ) ;
#85634=AXIS2_PLACEMENT_3D ( 'NONE', #179930, #200761, #61251 ) ;
#85682=DIRECTION ( 'NONE',  ( 1.000000000000000000, 0.000000000000000000, 0.000000000000000000 ) ) ;
#85781=DIRECTION ( 'NONE',  ( -0.000000000000000000, 0.8814952561688430555, -0.4721928772777346239 ) ) ;
#86054=EDGE_CURVE ( 'NONE', #192047, #112332, #57868, .T. ) ;
#86273=DIRECTION ( 'NONE',  ( 0.5932847527679298016, -0.3801118060259217613, -0.7095972217059537401 ) ) ;
#86588=FACE_OUTER_BOUND ( 'NONE', #149269, .T. ) ;
#86668=DIRECTION ( 'NONE',  ( 1.000000000000000000, 0.000000000000000000, 0.000000000000000000 ) ) ;
#86771=ORIENTED_EDGE ( 'NONE', *, *, #45037, .F. ) ;
#86794=CARTESIAN_POINT ( 'NONE',  ( -16.27683809663750480, 19.69766786220170829, -229.8585047820796490 ) ) ;
#86875=CARTESIAN_POINT ( 'NONE',  ( -16.93255653858138388, 22.94068984415941159, -230.8600761695373080 ) ) ;
#86915=LINE ( 'NONE', #167794, #101366 ) ;
#86952=DIRECTION ( 'NONE',  ( 1.000000000000000000, 5.603460673774838784E-17, 1.046060675573451523E-16 ) ) ;
#86985=PLANE ( 'NONE',  #122875 ) ;
#86988=ORIENTED_EDGE ( 'NONE', *, *, #154775, .F. ) ;
#87405=CARTESIAN_POINT ( 'NONE',  ( -18.40000000000000213, 33.92263863280957992, -235.0698407953532012 ) ) ;
#87552=VERTEX_POINT ( 'NONE', #209002 ) ;
#87874=PLANE ( 'NONE',  #238852 ) ;
#87961=ORIENTED_EDGE ( 'NONE', *, *, #93825, .F. ) ;
#87963=CARTESIAN_POINT ( 'NONE',  ( -15.75000000000000355, 26.30888228346803004, -233.3999513616626587 ) ) ;
#87995=DIRECTION ( 'NONE',  ( 1.000000000000000000, -0.000000000000000000, -0.000000000000000000 ) ) ;
#88151=CARTESIAN_POINT ( 'NONE',  ( -16.93970660449832621, 22.92160253073273424, -230.8335271541670295 ) ) ;
#88287=VERTEX_POINT ( 'NONE', #222154 ) ;
#88319=ORIENTED_EDGE ( 'NONE', *, *, #250664, .F. ) ;
#89147=VERTEX_POINT ( 'NONE', #183751 ) ;
#89189=VERTEX_POINT ( 'NONE', #50631 ) ;
#89559=VERTEX_POINT ( 'NONE', #7360 ) ;
#89642=CARTESIAN_POINT ( 'NONE',  ( -16.94878442675511465, 30.25972311995205288, -234.7883080098580990 ) ) ;
#89902=VERTEX_POINT ( 'NONE', #21204 ) ;
#89980=CIRCLE ( 'NONE', #69174, 0.1000000000000075273 ) ;
#90350=CARTESIAN_POINT ( 'NONE',  ( -16.84793658983391396, 30.13259441044248277, -234.7675476393297345 ) ) ;
#90567=CARTESIAN_POINT ( 'NONE',  ( -16.77828822508139694, 22.98741874091696147, -230.9443501695940313 ) ) ;
#90587=EDGE_LOOP ( 'NONE', ( #131705, #189273, #164605, #32891, #15508, #213441, #147349, #34164, #151272, #220175 ) ) ;
#90648=CARTESIAN_POINT ( 'NONE',  ( 12.25000000000000000, 26.40960863751538312, -233.4539077120826107 ) ) ;
#90712=VECTOR ( 'NONE', #248403, 1000.000000000000000 ) ;
#90726=ORIENTED_EDGE ( 'NONE', *, *, #177322, .T. ) ;
#90871=LINE ( 'NONE', #68757, #119043 ) ;
#90903=CARTESIAN_POINT ( 'NONE',  ( -18.34374000495059676, 33.92263863280957281, -235.0698407953532296 ) ) ;
#91181=DIRECTION ( 'NONE',  ( 0.000000000000000000, 0.8814952561688430555, -0.4721928772777346239 ) ) ;
#91475=CARTESIAN_POINT ( 'NONE',  ( 20.73486653747088937, 18.94215925855735705, -231.2688971919497760 ) ) ;
#91793=ADVANCED_FACE ( 'NONE', ( #100099 ), #110390, .T. ) ;
#91888=CARTESIAN_POINT ( 'NONE',  ( -16.87331047859651179, 22.97806745954242302, -230.9350634111226270 ) ) ;
#91943=CARTESIAN_POINT ( 'NONE',  ( 12.25000000000000000, 26.30888228346803004, -233.3999513616626587 ) ) ;
#91992=EDGE_LOOP ( 'NONE', ( #6599, #138042, #174573, #135172, #171979, #98972, #234221, #190244, #114367 ) ) ;
#92069=EDGE_CURVE ( 'NONE', #136504, #50994, #123235, .T. ) ;
#92104=EDGE_CURVE ( 'NONE', #50994, #249547, #89980, .T. ) ;
#92144=ORIENTED_EDGE ( 'NONE', *, *, #169622, .T. ) ;
#92523=EDGE_CURVE ( 'NONE', #189014, #69020, #240322, .T. ) ;
#92645=AXIS2_PLACEMENT_3D ( 'NONE', #128664, #218434, #55491 ) ;
#92707=DIRECTION ( 'NONE',  ( 0.000000000000000000, -0.1905202255954249191, -0.9816832705303010220 ) ) ;
#92911=CARTESIAN_POINT ( 'NONE',  ( -16.78493211734302903, 30.19206623356038222, -234.8041291499450836 ) ) ;
#93106=DIRECTION ( 'NONE',  ( -1.000000000000000000, 0.000000000000000000, 0.000000000000000000 ) ) ;
#93169=( LENGTH_UNIT ( ) NAMED_UNIT ( * ) SI_UNIT ( .MILLI., .METRE. ) );
#93205=EDGE_LOOP ( 'NONE', ( #96036, #144737, #185555, #213300 ) ) ;
#93310=VERTEX_POINT ( 'NONE', #197770 ) ;
#93390=EDGE_CURVE ( 'NONE', #176836, #89559, #227145, .T. ) ;
#93417=PLANE ( 'NONE',  #234396 ) ;
#93471=EDGE_CURVE ( 'NONE', #42653, #128551, #198962, .T. ) ;
#93722=ORIENTED_EDGE ( 'NONE', *, *, #6954, .F. ) ;
#93737=ORIENTED_EDGE ( 'NONE', *, *, #118401, .F. ) ;
#93825=EDGE_CURVE ( 'NONE', #13346, #74153, #85139, .T. ) ;
#93960=CARTESIAN_POINT ( 'NONE',  ( 21.72449340488910252, 20.13867536412185189, -229.0352267540020819 ) ) ;
#93961=VECTOR ( 'NONE', #228995, 1000.000000000000000 ) ;
#94055=ORIENTED_EDGE ( 'NONE', *, *, #74095, .F. ) ;
#94164=DIRECTION ( 'NONE',  ( -0.000000000000000000, 0.8814952561688430555, -0.4721928772777346239 ) ) ;
#94346=CARTESIAN_POINT ( 'NONE',  ( -18.40000000000000213, 23.82801463864234037, -229.3483719500187306 ) ) ;
#94510=CARTESIAN_POINT ( 'NONE',  ( -17.29158576265542990, 22.08723780851632412, -229.9873656484244862 ) ) ;
#94583=DIRECTION ( 'NONE',  ( 1.000000000000000000, 0.000000000000000000, 0.000000000000000000 ) ) ;
#94845=CARTESIAN_POINT ( 'NONE',  ( 18.39999999999999503, 23.69729366125098835, -229.5924034189314682 ) ) ;
#94913=ADVANCED_FACE ( 'NONE', ( #44859 ), #252042, .T. ) ;
#94955=STYLED_ITEM ( 'NONE', ( #179071 ), #20540 ) ;
#94959=CLOSED_SHELL ( 'NONE', ( #61817, #203578, #167434, #59164, #246017, #114096, #124125, #232802, #162605, #191597, #85392, #103413, #85349, #71844, #231006, #35411, #211705, #244319, #68528, #128771, #107199, #83728, #48466, #120602, #237972, #94913, #198184, #121850, #6194, #111797, #229272, #54755, #188330, #91793, #228322, #438, #31503, #59019, #134815, #150870, #4604, #236946, #72942, #61663, #215669, #82706, #75321, #77343, #186495, #170325, #191731, #49682, #122838 ) ) ;
#94965=CARTESIAN_POINT ( 'NONE',  ( -18.39999999999999858, 20.76715588789282307, -228.0228088279911560 ) ) ;
#95026=ORIENTED_EDGE ( 'NONE', *, *, #223798, .F. ) ;
#95086=ORIENTED_EDGE ( 'NONE', *, *, #165004, .F. ) ;
#95493=CARTESIAN_POINT ( 'NONE',  ( -16.77431908686106610, 30.19186540481982206, -234.8040555917334302 ) ) ;
#95536=CARTESIAN_POINT ( 'NONE',  ( -16.97683809663752186, 23.64127277249475156, -231.2903243416350847 ) ) ;
#95573=ORIENTED_EDGE ( 'NONE', *, *, #18514, .T. ) ;
#95726=( NAMED_UNIT ( * ) PLANE_ANGLE_UNIT ( ) SI_UNIT ( $, .RADIAN. ) );
#95829=CARTESIAN_POINT ( 'NONE',  ( -21.65000000000000213, 18.70606281991846842, -231.7096448200342138 ) ) ;
#95859=DIRECTION ( 'NONE',  ( 0.000000000000000000, 0.8814952561688428334, -0.4721928772777349015 ) ) ;
#96036=ORIENTED_EDGE ( 'NONE', *, *, #5419, .T. ) ;
#96473=ORIENTED_EDGE ( 'NONE', *, *, #93390, .F. ) ;
#96984=FILL_AREA_STYLE ('',( #134842 ) ) ;
#97217=VERTEX_POINT ( 'NONE', #76446 ) ;
#97443=EDGE_CURVE ( 'NONE', #123629, #192047, #239831, .T. ) ;
#97519=ORIENTED_EDGE ( 'NONE', *, *, #143391, .T. ) ;
#97695=CARTESIAN_POINT ( 'NONE',  ( -17.05016517656152431, 22.99807563533816435, -230.9457812431605817 ) ) ;
#97699=CARTESIAN_POINT ( 'NONE',  ( -16.90128866880176517, 30.21929489460931961, -234.8096846487093501 ) ) ;
#97938=DIRECTION ( 'NONE',  ( 0.000000000000000000, 0.4721928772777346239, 0.8814952561688430555 ) ) ;
#98253=CARTESIAN_POINT ( 'NONE',  ( -16.85697194749116790, 23.20972200652296280, -231.1061839156225233 ) ) ;
#98506=ORIENTED_EDGE ( 'NONE', *, *, #100550, .T. ) ;
#98657=ORIENTED_EDGE ( 'NONE', *, *, #139451, .F. ) ;
#98779=CARTESIAN_POINT ( 'NONE',  ( -18.40000000000000213, 20.70659057908908096, -227.9750359040556873 ) ) ;
#98828=LINE ( 'NONE', #18044, #147668 ) ;
#98848=AXIS2_PLACEMENT_3D ( 'NONE', #223072, #139665, #183953 ) ;
#98972=ORIENTED_EDGE ( 'NONE', *, *, #238008, .F. ) ;
#99186=APPLICATION_CONTEXT ( 'automotive_design' ) ;
#99548=CARTESIAN_POINT ( 'NONE',  ( -16.83558968593875349, 22.98891442405298591, -230.9408738330689062 ) ) ;
#100099=FACE_OUTER_BOUND ( 'NONE', #102973, .T. ) ;
#100116=DIRECTION ( 'NONE',  ( 1.000000000000000000, 1.156482317317869556E-14, 3.083952846180985271E-14 ) ) ;
#100550=EDGE_CURVE ( 'NONE', #189014, #104609, #198156, .T. ) ;
#100621=EDGE_CURVE ( 'NONE', #5154, #223523, #81370, .T. ) ;
#100645=CARTESIAN_POINT ( 'NONE',  ( -16.94445028196808778, 22.96031635112858282, -230.8778361528912058 ) ) ;
#100947=VERTEX_POINT ( 'NONE', #72161 ) ;
#101004=CARTESIAN_POINT ( 'NONE',  ( 12.29592348164039528, 25.90710817316709580, -233.1781447626814838 ) ) ;
#101366=VECTOR ( 'NONE', #209451, 1000.000000000000000 ) ;
#101407=VERTEX_POINT ( 'NONE', #251755 ) ;
#101419=CYLINDRICAL_SURFACE ( 'NONE', #252244, 1.749999999999999778 ) ;
#101558=CARTESIAN_POINT ( 'NONE',  ( -16.88593481969334320, 30.20824341629028709, -234.8074353544413100 ) ) ;
#101653=LINE ( 'NONE', #78260, #44160 ) ;
#101982=ORIENTED_EDGE ( 'NONE', *, *, #4222, .F. ) ;
#102098=ORIENTED_EDGE ( 'NONE', *, *, #154775, .T. ) ;
#102184=LINE ( 'NONE', #197461, #113314 ) ;
#102452=CARTESIAN_POINT ( 'NONE',  ( -12.26136940704872380, 26.51187484352280777, -233.5070971077067838 ) ) ;
#102599=VERTEX_POINT ( 'NONE', #168467 ) ;
#102639=PLANE ( 'NONE',  #158227 ) ;
#102851=CARTESIAN_POINT ( 'NONE',  ( -18.40000000000000213, 23.63051550414076729, -229.7170656735756324 ) ) ;
#102912=CARTESIAN_POINT ( 'NONE',  ( 18.39999999999999503, 30.92555476183550311, -233.4643850126089148 ) ) ;
#102973=EDGE_LOOP ( 'NONE', ( #210861, #162232 ) ) ;
#103079=CARTESIAN_POINT ( 'NONE',  ( -16.94333152886236959, 22.96006607477043104, -230.8796551298197528 ) ) ;
#103146=CARTESIAN_POINT ( 'NONE',  ( 18.39999999999997371, 20.83093076766827423, -227.7429161672744442 ) ) ;
#103353=EDGE_LOOP ( 'NONE', ( #125231, #250960 ) ) ;
#103397=CARTESIAN_POINT ( 'NONE',  ( -16.97683809663752186, 19.98098358856834977, -229.3296076283783407 ) ) ;
#103413=ADVANCED_FACE ( 'NONE', ( #60975 ), #80511, .F. ) ;
#103451=CARTESIAN_POINT ( 'NONE',  ( -17.11825945287482753, 23.06621698515930063, -230.9822826988504119 ) ) ;
#103509=VERTEX_POINT ( 'NONE', #205614 ) ;
#103740=CARTESIAN_POINT ( 'NONE',  ( -15.66061380678752535, 26.81104512947605656, -233.6567807927322917 ) ) ;
#103780=CARTESIAN_POINT ( 'NONE',  ( 15.69410316191958898, 26.71170214840295287, -233.6080780108829629 ) ) ;
#103785=CYLINDRICAL_SURFACE ( 'NONE', #253813, 1.749999999999999778 ) ;
#103956=VERTEX_POINT ( 'NONE', #94346 ) ;
#103984=VECTOR ( 'NONE', #25223, 1000.000000000000000 ) ;
#104116=EDGE_CURVE ( 'NONE', #178218, #46929, #189489, .T. ) ;
#104363=CARTESIAN_POINT ( 'NONE',  ( -16.94445028196808778, 22.96031635112858282, -230.8778361528912058 ) ) ;
#104376=ORIENTED_EDGE ( 'NONE', *, *, #93471, .T. ) ;
#104388=LINE ( 'NONE', #62728, #40680 ) ;
#104552=ORIENTED_EDGE ( 'NONE', *, *, #235174, .F. ) ;
#104609=VERTEX_POINT ( 'NONE', #196099 ) ;
#104666=CARTESIAN_POINT ( 'NONE',  ( -18.38817693311004575, 33.92657181652015908, -235.0624982814158841 ) ) ;
#104667=ORIENTED_EDGE ( 'NONE', *, *, #251366, .T. ) ;
#105006=CARTESIAN_POINT ( 'NONE',  ( -14.77538296656415007, 27.73642831988484758, -234.0663351390819287 ) ) ;
#105019=DIRECTION ( 'NONE',  ( -1.000000000000000000, 0.000000000000000000, 0.000000000000000000 ) ) ;
#105038=ORIENTED_EDGE ( 'NONE', *, *, #171497, .F. ) ;
#105051=DIRECTION ( 'NONE',  ( 1.000000000000000000, -9.458662978381124901E-16, 5.066746821047763994E-16 ) ) ;
#105291=PLANE ( 'NONE',  #125703 ) ;
#105472=DIRECTION ( 'NONE',  ( 1.186688945009009831E-16, -0.4721928772777346239, -0.8814952561688430555 ) ) ;
#105983=DIRECTION ( 'NONE',  ( -1.186688945009010324E-16, 0.4721928772777345684, 0.8814952561688430555 ) ) ;
#106512=CARTESIAN_POINT ( 'NONE',  ( -16.92570016628983609, 22.95634624765352427, -230.9134574420077968 ) ) ;
#107018=DIRECTION ( 'NONE',  ( 1.020425574104003999E-15, -0.8814952561688430555, 0.4721928772777346239 ) ) ;
#107199=ADVANCED_FACE ( 'NONE', ( #134896 ), #154531, .F. ) ;
#107461=DIRECTION ( 'NONE',  ( 0.000000000000000000, -0.8814952561688476074, 0.4721928772777262417 ) ) ;
#107477=CARTESIAN_POINT ( 'NONE',  ( 12.84233041328156943, 25.17626390180108231, -232.7245615205268052 ) ) ;
#107732=ORIENTED_EDGE ( 'NONE', *, *, #80736, .T. ) ;
#108639=CARTESIAN_POINT ( 'NONE',  ( -16.97683809663752896, 29.65845354706183201, -234.5135633587022426 ) ) ;
#108657=ORIENTED_EDGE ( 'NONE', *, *, #255365, .F. ) ;
#108724=ORIENTED_EDGE ( 'NONE', *, *, #14382, .T. ) ;
#108764=CARTESIAN_POINT ( 'NONE',  ( 14.56326696814970845, 24.89049957252425216, -232.5305204729232571 ) ) ;
#108832=CARTESIAN_POINT ( 'NONE',  ( -14.56556274378147542, 24.89114276590144925, -232.5309687781013395 ) ) ;
#108846=EDGE_CURVE ( 'NONE', #103509, #245289, #51852, .T. ) ;
#108849=CIRCLE ( 'NONE', #71474, 0.1000000000000013933 ) ;
#108947=VERTEX_POINT ( 'NONE', #257717 ) ;
#109206=CARTESIAN_POINT ( 'NONE',  ( -16.86445178670663481, 30.24803992267471742, -234.8155353274968604 ) ) ;
#109493=B_SPLINE_CURVE_WITH_KNOTS ( 'NONE', 3,
 ( #23858, #241588, #147623, #188045, #126777, #165930, #9388, #203749, #221996, #145045, #164628, #146326, #206322, #48520 ),
 .UNSPECIFIED., .F., .F.,
 ( 4, 2, 2, 2, 2, 2, 4 ),
 ( 0.000000000000000000, 2.389617747646909451E-05, 4.779235495293818902E-05, 9.558470990583940675E-05, 0.0001911694198115973086, 0.0003823388396230649466, 0.0007646776792459603241 ),
 .UNSPECIFIED. ) ;
#109666=PLANE ( 'NONE',  #115057 ) ;
#109775=VERTEX_POINT ( 'NONE', #39430 ) ;
#109782=CIRCLE ( 'NONE', #247145, 0.9000000000000014655 ) ;
#109905=CARTESIAN_POINT ( 'NONE',  ( -16.83199318825829849, 30.08928172373351728, -234.7663019489722842 ) ) ;
#109913=CARTESIAN_POINT ( 'NONE',  ( -16.87683809663752399, 29.49590395944697363, -234.5399335999045718 ) ) ;
#110217=CARTESIAN_POINT ( 'NONE',  ( 13.43663047529820176, 27.81851053932208728, -234.0989799278904115 ) ) ;
#110334=EDGE_CURVE ( 'NONE', #89902, #88287, #152021, .T. ) ;
#110390=PLANE ( 'NONE',  #123134 ) ;
#110540=CARTESIAN_POINT ( 'NONE',  ( -16.87845715379269507, 22.95868340314714118, -230.9157653750406496 ) ) ;
#110882=CARTESIAN_POINT ( 'NONE',  ( -17.11825945287481332, 30.25354784785470486, -234.7188954791831748 ) ) ;
#110961=EDGE_CURVE ( 'NONE', #87552, #67930, #65873, .T. ) ;
#111068=ORIENTED_EDGE ( 'NONE', *, *, #100621, .F. ) ;
#111269=EDGE_LOOP ( 'NONE', ( #55196, #49397, #164548 ) ) ;
#111394=EDGE_CURVE ( 'NONE', #69020, #25903, #155137, .T. ) ;
#111438=CARTESIAN_POINT ( 'NONE',  ( -17.01825945287482966, 23.02528674727019364, -230.8469138855057281 ) ) ;
#111498=VECTOR ( 'NONE', #212890, 1000.000000000000114 ) ;
#111607=CARTESIAN_POINT ( 'NONE',  ( -16.94037747912386394, 22.92091771185253535, -230.8323684894537848 ) ) ;
#111649=CARTESIAN_POINT ( 'NONE',  ( -20.65000000000000568, 21.70314669089253812, -233.3151006027785286 ) ) ;
#111718=FACE_OUTER_BOUND ( 'NONE', #123659, .T. ) ;
#111741=VERTEX_POINT ( 'NONE', #226603 ) ;
#111797=ADVANCED_FACE ( 'NONE', ( #117894 ), #197430, .F. ) ;
#111857=VECTOR ( 'NONE', #246604, 1000.000000000000000 ) ;
#111982=DIRECTION ( 'NONE',  ( 0.000000000000000000, 0.8814952561688476074, -0.4721928772777262417 ) ) ;
#112093=EDGE_CURVE ( 'NONE', #34727, #93310, #253249, .T. ) ;
#112236=CARTESIAN_POINT ( 'NONE',  ( -16.92209698673484297, 30.15287859541585291, -234.7784133219286105 ) ) ;
#112275=CARTESIAN_POINT ( 'NONE',  ( -16.27683809663751191, 19.69766786220167631, -229.8585047820796490 ) ) ;
#112332=VERTEX_POINT ( 'NONE', #110882 ) ;
#112509=CARTESIAN_POINT ( 'NONE',  ( -16.87683809663752044, 29.54312324717474780, -234.4517840742876729 ) ) ;
#112745=PRESENTATION_STYLE_ASSIGNMENT (( #16236 ) ) ;
#112801=CARTESIAN_POINT ( 'NONE',  ( 13.22461703343584816, 27.73642831988484758, -234.0663351390819571 ) ) ;
#112866=CARTESIAN_POINT ( 'NONE',  ( -33.72168855820451938, 30.20632856012699108, -234.8070450048000737 ) ) ;
#112940=ORIENTED_EDGE ( 'NONE', *, *, #234528, .F. ) ;
#113107=CARTESIAN_POINT ( 'NONE',  ( -18.34374000495059676, 33.92263863280957281, -235.0698407953532296 ) ) ;
#113224=PRODUCT_DEFINITION_CONTEXT ( 'detailed design', #99186, 'design' ) ;
#113314=VECTOR ( 'NONE', #181766, 1000.000000000000000 ) ;
#113499=CARTESIAN_POINT ( 'NONE',  ( -16.97092634996718274, 30.24786202487886300, -234.7715630666886568 ) ) ;
#113802=CARTESIAN_POINT ( 'NONE',  ( -21.64999999999999858, 30.25354784785470486, -234.7188954791831748 ) ) ;
#113856=LINE ( 'NONE', #133426, #118993 ) ;
#113907=CARTESIAN_POINT ( 'NONE',  ( -16.89268316805466341, 22.97380970494227626, -230.9308293615217451 ) ) ;
#113948=ORIENTED_EDGE ( 'NONE', *, *, #115411, .F. ) ;
#113967=CARTESIAN_POINT ( 'NONE',  ( -12.47155713865591231, 25.54333932933834106, -232.9607505220590156 ) ) ;
#114096=ADVANCED_FACE ( 'NONE', ( #894 ), #178310, .F. ) ;
#114141=CIRCLE ( 'NONE', #64270, 0.1000000000000013933 ) ;
#114150=FACE_BOUND ( 'NONE', #184147, .T. ) ;
#114346=CARTESIAN_POINT ( 'NONE',  ( -16.86337532320260735, 30.30768031064097912, -234.8273404860777873 ) ) ;
#114367=ORIENTED_EDGE ( 'NONE', *, *, #188646, .F. ) ;
#114448=CIRCLE ( 'NONE', #122842, 0.5000000000000004441 ) ;
#114841=CARTESIAN_POINT ( 'NONE',  ( -16.94107738177415357, 22.92025126680846014, -230.8312174982872591 ) ) ;
#115041=EDGE_CURVE ( 'NONE', #195949, #18361, #109782, .T. ) ;
#115057=AXIS2_PLACEMENT_3D ( 'NONE', #93960, #74447, #75704 ) ;
#115059=CARTESIAN_POINT ( 'NONE',  ( 18.39999999999999503, 20.94763808724815846, -234.7254930126486556 ) ) ;
#115111=ORIENTED_EDGE ( 'NONE', *, *, #247167, .T. ) ;
#115411=EDGE_CURVE ( 'NONE', #196055, #111741, #171809, .T. ) ;
#115553=ORIENTED_EDGE ( 'NONE', *, *, #19684, .F. ) ;
#115665=EDGE_LOOP ( 'NONE', ( #253652, #86988, #117476, #64292, #96473 ) ) ;
#115808=ORIENTED_EDGE ( 'NONE', *, *, #159478, .F. ) ;
#115826=ORIENTED_EDGE ( 'NONE', *, *, #166988, .T. ) ;
#115931=CYLINDRICAL_SURFACE ( 'NONE', #4464, 0.1000000000000013933 ) ;
#116246=ORIENTED_EDGE ( 'NONE', *, *, #179507, .F. ) ;
#116621=CARTESIAN_POINT ( 'NONE',  ( -18.40000000000000213, 20.94763808724815846, -234.7254930126486556 ) ) ;
#116732=CARTESIAN_POINT ( 'NONE',  ( -16.77828822459933633, 30.19341635460695983, -234.8044058226641653 ) ) ;
#116859=ORIENTED_EDGE ( 'NONE', *, *, #223015, .T. ) ;
#117158=DIRECTION ( 'NONE',  ( -1.000000000000000000, 0.000000000000000000, 0.000000000000000000 ) ) ;
#117295=CARTESIAN_POINT ( 'NONE',  ( -17.01764560440512852, 23.06621698446732083, -230.9822826984797359 ) ) ;
#117476=ORIENTED_EDGE ( 'NONE', *, *, #200262, .F. ) ;
#117799=VERTEX_POINT ( 'NONE', #122045 ) ;
#117894=FACE_OUTER_BOUND ( 'NONE', #209671, .T. ) ;
#117964=( BOUNDED_CURVE ( )  B_SPLINE_CURVE ( 3, ( #23962, #142581, #206426, #103451 ),
 .UNSPECIFIED., .F., .F. ) 
 B_SPLINE_CURVE_WITH_KNOTS ( ( 4, 4 ),
 ( 0.5235987755983078085, 1.570796326794896558 ),
 .UNSPECIFIED. ) 
 CURVE ( )  GEOMETRIC_REPRESENTATION_ITEM ( )  RATIONAL_B_SPLINE_CURVE ( ( 1.000000000000000000, 0.9106836025229606557, 0.9106836025229606557, 1.000000000000000000 ) ) 
 REPRESENTATION_ITEM ( '' )  );
#118191=CARTESIAN_POINT ( 'NONE',  ( -16.87036670365548474, 30.33914847462231279, -234.8334748671511818 ) ) ;
#118333=VERTEX_POINT ( 'NONE', #177235 ) ;
#118401=EDGE_CURVE ( 'NONE', #111741, #196055, #154052, .T. ) ;
#118431=VERTEX_POINT ( 'NONE', #91888 ) ;
#118626=AXIS2_PLACEMENT_3D ( 'NONE', #35098, #91181, #191599 ) ;
#118977=CARTESIAN_POINT ( 'NONE',  ( 18.39999999999999503, 23.82801463864234037, -229.3483719500187306 ) ) ;
#118993=VECTOR ( 'NONE', #195984, 1000.000000000000000 ) ;
#119043=VECTOR ( 'NONE', #191297, 1000.000000000000000 ) ;
#119154=CARTESIAN_POINT ( 'NONE',  ( -16.97683810757273193, 23.51893242087254166, -231.2247899644102631 ) ) ;
#119224=DIRECTION ( 'NONE',  ( -1.020425574104003999E-15, -0.8814952561688430555, 0.4721928772777346239 ) ) ;
#119484=B_SPLINE_CURVE_WITH_KNOTS ( 'NONE', 3,
 ( #94965, #177107, #223883, #98779 ),
 .UNSPECIFIED., .F., .F.,
 ( 4, 4 ),
 ( 0.000000000000000000, 7.713889350928795333E-05 ),
 .UNSPECIFIED. ) ;
#119499=CARTESIAN_POINT ( 'NONE',  ( -12.30589683808041279, 26.71170214840295642, -233.6080780108829344 ) ) ;
#119516=( BOUNDED_SURFACE ( )  B_SPLINE_SURFACE ( 3, 2, ( 
 ( #254753, #76154, #175303 ),
 ( #119154, #77425, #137411 ),
 ( #39643, #154459, #20061 ),
 ( #59132, #235237, #98253 ),
 ( #257312, #194857, #56566 ),
 ( #233954, #139965, #219516 ),
 ( #218217, #215658, #78713 ),
 ( #99548, #179153, #74915 ),
 ( #239099, #55281, #216944 ),
 ( #462, #79986, #134826 ) ),
 .UNSPECIFIED., .F., .F., .F. ) 
 B_SPLINE_SURFACE_WITH_KNOTS ( ( 4, 2, 2, 2, 4 ),
 ( 3, 3 ),
 ( 0.002161241639767790771, 0.002579950749617455040, 0.002789305304542286958, 0.002893982582004702916, 0.002998659859467118875 ),
 ( 0.000000000000000000, 1.000000000000000000 ),
 .UNSPECIFIED. ) 
 GEOMETRIC_REPRESENTATION_ITEM ( )  RATIONAL_B_SPLINE_SURFACE ( (
 ( 1.000000000000000000, 0.7071067811864378827, 1.000000000000000000),
 ( 1.000000000000000000, 0.7632447400650679281, 1.000000000000000000),
 ( 1.000000000000000000, 0.8158073005128387845, 1.000000000000000000),
 ( 1.000000000000000000, 0.8906973462385610052, 1.000000000000000000),
 ( 1.000000000000000000, 0.9149408947793243874, 1.000000000000000000),
 ( 1.000000000000000000, 0.9493368785279177047, 1.000000000000000000),
 ( 1.000000000000000000, 0.9605194247156390031, 1.000000000000000000),
 ( 1.000000000000000000, 0.9803630264780962555, 1.000000000000000000),
 ( 1.000000000000000000, 0.9900844824271249900, 1.000000000000000000),
 ( 1.000000000000000000, 0.9894588281429297361, 1.000000000000000000) ) ) 
 REPRESENTATION_ITEM ( '' )  SURFACE ( )  );
#119892=CARTESIAN_POINT ( 'NONE',  ( -16.94275863006528482, 30.26173435748351537, -234.7919186320798985 ) ) ;
#119903=AXIS2_PLACEMENT_3D ( 'NONE', #3537, #63506, #20567 ) ;
#120139=ORIENTED_EDGE ( 'NONE', *, *, #172983, .F. ) ;
#120508=ORIENTED_EDGE ( 'NONE', *, *, #223015, .F. ) ;
#120561=DIRECTION ( 'NONE',  ( 0.000000000000000000, -0.4721928772777346239, -0.8814952561688430555 ) ) ;
#120602=ADVANCED_FACE ( 'NONE', ( #62488 ), #142005, .F. ) ;
#120647=CARTESIAN_POINT ( 'NONE',  ( 12.25000000000000000, 26.10747769360537873, -233.2920644364425300 ) ) ;
#120689=ORIENTED_EDGE ( 'NONE', *, *, #50571, .F. ) ;
#120989=DIRECTION ( 'NONE',  ( 0.000000000000000000, -0.8814952561688429444, 0.4721928772777345684 ) ) ;
#121027=CARTESIAN_POINT ( 'NONE',  ( -16.81744102076748959, 30.20632856012693424, -234.8070450048000737 ) ) ;
#121180=FACE_OUTER_BOUND ( 'NONE', #19703, .T. ) ;
#121303=CARTESIAN_POINT ( 'NONE',  ( 23.24999999999999645, 23.82801463864234393, -229.3483719500187306 ) ) ;
#121850=ADVANCED_FACE ( 'NONE', ( #86588 ), #87874, .F. ) ;
#122036=CARTESIAN_POINT ( 'NONE',  ( 16.87683809663749557, 30.20632856012693068, -234.8070450048000737 ) ) ;
#122045=CARTESIAN_POINT ( 'NONE',  ( -23.25000000000000355, 28.17589918783267322, -238.5974746063260739 ) ) ;
#122061=CARTESIAN_POINT ( 'NONE',  ( -14.87770893841226894, 27.68529808098225686, -234.0457819887453468 ) ) ;
#122206=VERTEX_POINT ( 'NONE', #126725 ) ;
#122242=DIRECTION ( 'NONE',  ( 1.186688945009010324E-16, -0.4721928772777346239, -0.8814952561688430555 ) ) ;
#122692=CARTESIAN_POINT ( 'NONE',  ( -16.94275863009466576, 22.95996116793751085, -230.8805586247883639 ) ) ;
#122838=ADVANCED_FACE ( 'NONE', ( #212386 ), #19302, .T. ) ;
#122842=AXIS2_PLACEMENT_3D ( 'NONE', #135181, #20402, #38669 ) ;
#122875=AXIS2_PLACEMENT_3D ( 'NONE', #150839, #126125, #131275 ) ;
#122901=FACE_OUTER_BOUND ( 'NONE', #141790, .T. ) ;
#123077=CARTESIAN_POINT ( 'NONE',  ( -16.85939681242906474, 29.91185388629861563, -234.7000971468440298 ) ) ;
#123134=AXIS2_PLACEMENT_3D ( 'NONE', #11302, #189938, #86952 ) ;
#123147=VECTOR ( 'NONE', #105051, 1000.000000000000000 ) ;
#123173=CIRCLE ( 'NONE', #227210, 0.9000000000000014655 ) ;
#123235=LINE ( 'NONE', #179378, #81390 ) ;
#123345=CARTESIAN_POINT ( 'NONE',  ( -12.48127053791145258, 27.09445758862755227, -233.7906081272070082 ) ) ;
#123379=CARTESIAN_POINT ( 'NONE',  ( 15.74999999999999645, 26.41090933635396354, -233.4546044608430577 ) ) ;
#123546=DIRECTION ( 'NONE',  ( -1.073024830501117528E-15, 0.8814952561688430555, -0.4721928772777346239 ) ) ;
#123587=DIRECTION ( 'NONE',  ( -1.000000000000000000, 0.000000000000000000, 0.000000000000000000 ) ) ;
#123601=ORIENTED_EDGE ( 'NONE', *, *, #23186, .T. ) ;
#123629=VERTEX_POINT ( 'NONE', #239999 ) ;
#123659=EDGE_LOOP ( 'NONE', ( #112940, #203782, #168048, #49896, #251862, #43247, #134056, #142403, #27046 ) ) ;
#124076=CARTESIAN_POINT ( 'NONE',  ( -21.64999999999999858, 29.92301283376028920, -235.3359421585013820 ) ) ;
#124125=ADVANCED_FACE ( 'NONE', ( #111718 ), #86985, .F. ) ;
#124308=LINE ( 'NONE', #203831, #103984 ) ;
#124652=AXIS2_PLACEMENT_3D ( 'NONE', #76879, #14380, #156468 ) ;
#124669=DIRECTION ( 'NONE',  ( 0.000000000000000000, 0.8814952561688429444, -0.4721928772777345684 ) ) ;
#124681=CARTESIAN_POINT ( 'NONE',  ( -16.90987985657661241, 30.22701669195686591, -234.8092699405564190 ) ) ;
#124731=CARTESIAN_POINT ( 'NONE',  ( -16.86132326855787511, 23.02093967300761079, -230.9580288822238003 ) ) ;
#124788=( BOUNDED_CURVE ( )  B_SPLINE_CURVE ( 3, ( #152550, #153851, #252889, #166005 ),
 .UNSPECIFIED., .F., .F. ) 
 B_SPLINE_CURVE_WITH_KNOTS ( ( 4, 4 ),
 ( 3.752122642744585956, 4.712388980384673687 ),
 .UNSPECIFIED. ) 
 CURVE ( )  GEOMETRIC_REPRESENTATION_ITEM ( )  RATIONAL_B_SPLINE_CURVE ( ( 1.000000000000000000, 0.9246222802177221922, 0.9246222802177221922, 1.000000000000000000 ) ) 
 REPRESENTATION_ITEM ( '' )  );
#124890=VECTOR ( 'NONE', #57398, 1000.000000000000000 ) ;
#124932=VERTEX_POINT ( 'NONE', #131628 ) ;
#125231=ORIENTED_EDGE ( 'NONE', *, *, #160121, .T. ) ;
#125240=DIRECTION ( 'NONE',  ( 0.000000000000000000, 0.4721928772777346239, 0.8814952561688430555 ) ) ;
#125241=CARTESIAN_POINT ( 'NONE',  ( -16.92925196614876171, 22.95929811576328916, -230.8996751924844659 ) ) ;
#125414=VECTOR ( 'NONE', #120561, 1000.000000000000000 ) ;
#125503=VERTEX_POINT ( 'NONE', #227025 ) ;
#125634=CARTESIAN_POINT ( 'NONE',  ( -20.65000000000000568, 28.93140779147704933, -237.1870821964559184 ) ) ;
#125703=AXIS2_PLACEMENT_3D ( 'NONE', #247396, #248697, #243553 ) ;
#126084=CARTESIAN_POINT ( 'NONE',  ( -16.94878442675512176, 22.96408127013238598, -230.8802323934030767 ) ) ;
#126125=DIRECTION ( 'NONE',  ( 0.000000000000000000, 0.8814952561688430555, -0.4721928772777346239 ) ) ;
#126138=ORIENTED_EDGE ( 'NONE', *, *, #191991, .F. ) ;
#126142=VECTOR ( 'NONE', #135939, 1000.000000000000000 ) ;
#126308=( BOUNDED_CURVE ( )  B_SPLINE_CURVE ( 3, ( #122036, #46330, #201558, #222380 ),
 .UNSPECIFIED., .F., .F. ) 
 B_SPLINE_CURVE_WITH_KNOTS ( ( 4, 4 ),
 ( 3.432212674861196966, 3.693332928900582068 ),
 .UNSPECIFIED. ) 
 CURVE ( )  GEOMETRIC_REPRESENTATION_ITEM ( )  RATIONAL_B_SPLINE_CURVE ( ( 1.000000000000000000, 0.9943260843901261525, 0.9943260843901261525, 1.000000000000000000 ) ) 
 REPRESENTATION_ITEM ( '' )  );
#126588=ORIENTED_EDGE ( 'NONE', *, *, #51930, .T. ) ;
#126713=LINE ( 'NONE', #206254, #180821 ) ;
#126725=CARTESIAN_POINT ( 'NONE',  ( 22.88900146558018989, 29.61793127808049775, -235.9054720201688156 ) ) ;
#126777=CARTESIAN_POINT ( 'NONE',  ( -16.80468759584939775, 23.00963892154194923, -230.9608765328473226 ) ) ;
#126892=PLANE ( 'NONE',  #248572 ) ;
#127044=CARTESIAN_POINT ( 'NONE',  ( 13.76927104934458157, 24.82647667088539833, -232.4856315176584474 ) ) ;
#127227=CARTESIAN_POINT ( 'NONE',  ( -18.34804628011471195, 20.70020979027686892, -227.9869476361872955 ) ) ;
#127538=CARTESIAN_POINT ( 'NONE',  ( -16.87036670365548474, 30.33914847462231279, -234.8334748671511818 ) ) ;
#127620=ORIENTED_EDGE ( 'NONE', *, *, #161860, .T. ) ;
#127753=CARTESIAN_POINT ( 'NONE',  ( -18.40000000000000213, 20.94763808724815846, -234.7254930126486556 ) ) ;
#128177=DIRECTION ( 'NONE',  ( 1.000000000000000000, 5.603460673774837551E-17, 1.046060675573451153E-16 ) ) ;
#128211=CARTESIAN_POINT ( 'NONE',  ( -16.84419801905645642, 30.18914835313876210, -234.7978420382347906 ) ) ;
#128342=CARTESIAN_POINT ( 'NONE',  ( 14.11444803880196197, 24.81692076904265321, -232.4788742220511608 ) ) ;
#128511=CARTESIAN_POINT ( 'NONE',  ( 12.42718393586866732, 27.00251997126095560, -233.7480822475820048 ) ) ;
#128551=VERTEX_POINT ( 'NONE', #44850 ) ;
#128636=EDGE_CURVE ( 'NONE', #97217, #12088, #14739, .T. ) ;
#128645=UNCERTAINTY_MEASURE_WITH_UNIT (LENGTH_MEASURE( 1.000000000000000082E-05 ), #93169, 'distance_accuracy_value', 'NONE');
#128664=CARTESIAN_POINT ( 'NONE',  ( -21.64999999999999858, 19.69766786220170829, -229.8585047820796490 ) ) ;
#128771=ADVANCED_FACE ( 'NONE', ( #134784 ), #31887, .T. ) ;
#128831=AXIS2_PLACEMENT_3D ( 'NONE', #194558, #14629, #135819 ) ;
#128836=ORIENTED_EDGE ( 'NONE', *, *, #213328, .F. ) ;
#129618=CARTESIAN_POINT ( 'NONE',  ( 13.88302573338719448, 24.81705829073095515, -232.4789712399791313 ) ) ;
#129722=VECTOR ( 'NONE', #239911, 1000.000000000000000 ) ;
#129927=CARTESIAN_POINT ( 'NONE',  ( 15.74999999999999645, 26.54497872210689735, -232.9592037335782209 ) ) ;
#130191=CYLINDRICAL_SURFACE ( 'NONE', #194032, 1.749999999999998002 ) ;
#130487=LINE ( 'NONE', #212616, #20107 ) ;
#130701=CARTESIAN_POINT ( 'NONE',  ( -16.77683809663752257, 33.06517536918362055, -220.7872234046467952 ) ) ;
#131275=DIRECTION ( 'NONE',  ( -1.000000000000000000, 0.000000000000000000, 0.000000000000000000 ) ) ;
#131415=AXIS2_PLACEMENT_3D ( 'NONE', #140503, #220062, #120989 ) ;
#131628=CARTESIAN_POINT ( 'NONE',  ( 20.05000000000002913, 28.93140779147706354, -237.1870821964558900 ) ) ;
#131671=DIRECTION ( 'NONE',  ( 0.000000000000000000, 0.8814952561688429444, -0.4721928772777345684 ) ) ;
#131705=ORIENTED_EDGE ( 'NONE', *, *, #77474, .F. ) ;
#132054=CARTESIAN_POINT ( 'NONE',  ( -16.80469485234342741, 30.16733359419953686, -234.7950599053594658 ) ) ;
#132058=CARTESIAN_POINT ( 'NONE',  ( -16.85697194749117145, 29.93552328732817003, -234.7090115389776201 ) ) ;
#132321=CARTESIAN_POINT ( 'NONE',  ( -16.87683809663752399, 33.06517536918362055, -220.7872234046467952 ) ) ;
#132354=CARTESIAN_POINT ( 'NONE',  ( 12.26145404764308822, 26.51259657475388920, -233.5074718021644458 ) ) ;
#132379=( GEOMETRIC_REPRESENTATION_CONTEXT ( 3 ) GLOBAL_UNCERTAINTY_ASSIGNED_CONTEXT ( ( #62308 ) ) GLOBAL_UNIT_ASSIGNED_CONTEXT ( ( #137322, #197303, #39565 ) ) REPRESENTATION_CONTEXT ( 'NONE', 'WORKASPACE' ) );
#132712=DIRECTION ( 'NONE',  ( 0.000000000000000000, -0.8814952561688430555, 0.4721928772777346239 ) ) ;
#132775=DIRECTION ( 'NONE',  ( -3.035766082959430086E-14, 0.8814952561688430555, -0.4721928772777346239 ) ) ;
#133180=B_SPLINE_CURVE_WITH_KNOTS ( 'NONE', 3,
 ( #5656, #128211, #245592, #147779, #33009, #209027, #206456, #29152, #108639, #227297 ),
 .UNSPECIFIED., .F., .F.,
 ( 4, 2, 2, 2, 4 ),
 ( 5.248391470688752094E-16, 9.930191194500769870E-05, 0.0001986038238894905622, 0.0003972076477784563164, 0.0007944152955563376804 ),
 .UNSPECIFIED. ) ;
#133265=CARTESIAN_POINT ( 'NONE',  ( -17.78241384938698744, 32.75037188247295461, -235.1425015842832806 ) ) ;
#133403=ORIENTED_EDGE ( 'NONE', *, *, #177976, .T. ) ;
#133426=CARTESIAN_POINT ( 'NONE',  ( -18.40000000000000213, 28.17589918783267322, -238.5974746063260739 ) ) ;
#133539=VERTEX_POINT ( 'NONE', #129927 ) ;
#133540=CARTESIAN_POINT ( 'NONE',  ( -13.22483237240078857, 24.96309550270879640, -232.5807238286746497 ) ) ;
#133693=DIRECTION ( 'NONE',  ( 0.000000000000000000, -0.4721928772777346239, -0.8814952561688430555 ) ) ;
#133918=DIRECTION ( 'NONE',  ( -0.000000000000000000, 0.8814952561688430555, -0.4721928772777346239 ) ) ;
#134056=ORIENTED_EDGE ( 'NONE', *, *, #213643, .F. ) ;
#134315=DIRECTION ( 'NONE',  ( 1.186688945009009831E-16, -0.4721928772777346239, -0.8814952561688430555 ) ) ;
#134514=EDGE_CURVE ( 'NONE', #239889, #26637, #177163, .T. ) ;
#134564=CARTESIAN_POINT ( 'NONE',  ( 21.13736287352038445, 19.08223167578460533, -231.0074083443886366 ) ) ;
#134722=ORIENTED_EDGE ( 'NONE', *, *, #52700, .T. ) ;
#134784=FACE_OUTER_BOUND ( 'NONE', #246163, .T. ) ;
#134815=ADVANCED_FACE ( 'NONE', ( #209525 ), #93417, .T. ) ;
#134826=CARTESIAN_POINT ( 'NONE',  ( -16.77431908686106610, 22.98856962916521240, -230.9454472391804813 ) ) ;
#134842=FILL_AREA_STYLE_COLOUR ( '', #64427 ) ;
#134896=FACE_OUTER_BOUND ( 'NONE', #203508, .T. ) ;
#134929=VECTOR ( 'NONE', #133918, 1000.000000000000000 ) ;
#135043=CARTESIAN_POINT ( 'NONE',  ( -16.87331047859649757, 30.20632856012693424, -234.8070450048000737 ) ) ;
#135160=DIRECTION ( 'NONE',  ( 0.000000000000000000, 0.000000000000000000, 1.000000000000000000 ) ) ;
#135172=ORIENTED_EDGE ( 'NONE', *, *, #227232, .F. ) ;
#135181=CARTESIAN_POINT ( 'NONE',  ( 20.73486653747088937, 29.16750423011593440, -236.7463345683714522 ) ) ;
#135282=CARTESIAN_POINT ( 'NONE',  ( -16.97683809663752186, 23.64127277249475156, -231.2903243416350847 ) ) ;
#135438=LINE ( 'NONE', #235825, #161282 ) ;
#135503=CARTESIAN_POINT ( 'NONE',  ( 23.24999999999999645, 29.67396024497139706, -235.8008764811443712 ) ) ;
#135549=ORIENTED_EDGE ( 'NONE', *, *, #212473, .T. ) ;
#135617=CARTESIAN_POINT ( 'NONE',  ( -16.87242674293849376, 30.20728960713221767, -234.8075598113715898 ) ) ;
#135671=CARTESIAN_POINT ( 'NONE',  ( -16.91256925476570672, 22.89123816192538285, -230.8480166193616867 ) ) ;
#135819=DIRECTION ( 'NONE',  ( 0.000000000000000000, -0.8814952561688429444, 0.4721928772777345684 ) ) ;
#135863=CARTESIAN_POINT ( 'NONE',  ( 21.72449340488910252, 23.13575923509592513, -230.6406825367463966 ) ) ;
#135939=DIRECTION ( 'NONE',  ( -1.000000000000000000, -9.458662978381124901E-16, 5.066746821047763994E-16 ) ) ;
#135961=EDGE_CURVE ( 'NONE', #112332, #173445, #114141, .T. ) ;
#136159=EDGE_LOOP ( 'NONE', ( #116246, #165703, #176817, #78696 ) ) ;
#136273=DIRECTION ( 'NONE',  ( 0.2834754621636438876, 0.6737039339378290137, -0.6824695390622222968 ) ) ;
#136305=DIRECTION ( 'NONE',  ( 1.186688945009009831E-16, -0.4721928772777346239, -0.8814952561688430555 ) ) ;
#136314=ORIENTED_EDGE ( 'NONE', *, *, #215485, .T. ) ;
#136442=CARTESIAN_POINT ( 'NONE',  ( -16.86420534634261514, 30.27630137067296090, -234.8211406191147717 ) ) ;
#136487=B_SPLINE_CURVE_WITH_KNOTS ( 'NONE', 3,
 ( #3126, #82650, #241754, #142642, #34835, #136442, #59457, #114346, #257632, #118191 ),
 .UNSPECIFIED., .F., .F.,
 ( 4, 3, 3, 4 ),
 ( 7.632826238684376041E-06, 4.756916949875301682E-05, 9.484459048150192589E-05, 0.0001435500935099878316 ),
 .UNSPECIFIED. ) ;
#136504=VERTEX_POINT ( 'NONE', #178358 ) ;
#136738=DIRECTION ( 'NONE',  ( 0.000000000000000000, 0.4721928772777346239, 0.8814952561688430555 ) ) ;
#137118=CARTESIAN_POINT ( 'NONE',  ( -17.22767730082000526, 31.53411859322281785, -235.0653887475340014 ) ) ;
#137205=VERTEX_POINT ( 'NONE', #154042 ) ;
#137232=DIRECTION ( 'NONE',  ( 0.000000000000000000, 0.4721928772777346239, 0.8814952561688430555 ) ) ;
#137297=ORIENTED_EDGE ( 'NONE', *, *, #5419, .F. ) ;
#137322=( LENGTH_UNIT ( ) NAMED_UNIT ( * ) SI_UNIT ( .MILLI., .METRE. ) );
#137354=ORIENTED_EDGE ( 'NONE', *, *, #233220, .T. ) ;
#137411=CARTESIAN_POINT ( 'NONE',  ( -16.87683809663752754, 23.48261004695467591, -231.3007506504703770 ) ) ;
#137799=VECTOR ( 'NONE', #59707, 1000.000000000000000 ) ;
#138033=CARTESIAN_POINT ( 'NONE',  ( -16.87683809663752399, 22.97806745954242302, -230.9350634111226270 ) ) ;
#138042=ORIENTED_EDGE ( 'NONE', *, *, #180233, .T. ) ;
#138114=CARTESIAN_POINT ( 'NONE',  ( -17.11825945287482753, 23.06621698515930419, -230.9822826988504119 ) ) ;
#138282=EDGE_LOOP ( 'NONE', ( #128836, #168660, #229529, #253115 ) ) ;
#138371=CARTESIAN_POINT ( 'NONE',  ( -17.80356949364322716, 32.72696218579464045, -235.1059619251321067 ) ) ;
#138574=ORIENTED_EDGE ( 'NONE', *, *, #199990, .T. ) ;
#138605=DIRECTION ( 'NONE',  ( 1.000000000000000000, 0.000000000000000000, 0.000000000000000000 ) ) ;
#138669=FACE_OUTER_BOUND ( 'NONE', #157142, .T. ) ;
#138901=DIRECTION ( 'NONE',  ( 0.000000000000000000, -0.4721928772776973204, -0.8814952561688629284 ) ) ;
#139112=CARTESIAN_POINT ( 'NONE',  ( -16.94225986326250677, 23.23962418155415577, -231.0751721868350330 ) ) ;
#139451=EDGE_CURVE ( 'NONE', #89189, #140686, #30444, .T. ) ;
#139452=DIRECTION ( 'NONE',  ( -0.000000000000000000, 0.8814952561688430555, -0.4721928772777346239 ) ) ;
#139465=CARTESIAN_POINT ( 'NONE',  ( -16.94445028196807002, 30.26380394232451465, -234.7901145182196956 ) ) ;
#139558=LINE ( 'NONE', #198260, #222501 ) ;
#139649=ORIENTED_EDGE ( 'NONE', *, *, #141900, .F. ) ;
#139665=DIRECTION ( 'NONE',  ( -1.073024830501117528E-15, 0.8814952561688430555, -0.4721928772777346239 ) ) ;
#139711=DIRECTION ( 'NONE',  ( 1.000000000000000000, 0.000000000000000000, 0.000000000000000000 ) ) ;
#139824=EDGE_LOOP ( 'NONE', ( #191833, #72295, #250455, #115808, #84825 ) ) ;
#139917=CIRCLE ( 'NONE', #152449, 0.09999999999999681366 ) ;
#139965=CARTESIAN_POINT ( 'NONE',  ( -16.85722902420145175, 23.07992200953330197, -230.9896241052242090 ) ) ;
#140010=DIRECTION ( 'NONE',  ( -1.020425574104003999E-15, 0.8814952561688429444, -0.4721928772777345684 ) ) ;
#140035=CARTESIAN_POINT ( 'NONE',  ( 18.39999999999999503, 23.82801463864234037, -229.3483719500187306 ) ) ;
#140137=LINE ( 'NONE', #200139, #185526 ) ;
#140217=EDGE_LOOP ( 'NONE', ( #169200, #102098, #18760 ) ) ;
#140423=CARTESIAN_POINT ( 'NONE',  ( -18.40000000000000213, 34.05335961020092128, -234.8258093264404351 ) ) ;
#140481=DIRECTION ( 'NONE',  ( 0.7071067811865462405, -0.3338907855510739875, -0.6233112732207629625 ) ) ;
#140503=CARTESIAN_POINT ( 'NONE',  ( 23.24999999999999645, 20.83093076766827423, -227.7429161672744442 ) ) ;
#140587=FACE_OUTER_BOUND ( 'NONE', #7865, .T. ) ;
#140686=VERTEX_POINT ( 'NONE', #33152 ) ;
#140908=AXIS2_PLACEMENT_3D ( 'NONE', #130701, #26489, #105983 ) ;
#141101=CARTESIAN_POINT ( 'NONE',  ( -16.98495255085919098, 22.99074469765236728, -230.8788200404308952 ) ) ;
#141239=CARTESIAN_POINT ( 'NONE',  ( -23.25000000000000355, 17.95055421627409231, -233.1200372299043693 ) ) ;
#141272=LINE ( 'NONE', #220803, #81404 ) ;
#141425=CARTESIAN_POINT ( 'NONE',  ( 20.27550659511089037, 22.63149853307782422, -231.5820423879664247 ) ) ;
#141506=DIRECTION ( 'NONE',  ( -1.000000000000000000, 7.801181613359275410E-16, 1.456333823655510085E-15 ) ) ;
#141551=DIRECTION ( 'NONE',  ( -0.000000000000000000, 0.8814952561688430555, -0.4721928772777346239 ) ) ;
#141612=CARTESIAN_POINT ( 'NONE',  ( -15.57281606413133979, 27.00251997126096271, -233.7480822475820332 ) ) ;
#141631=ORIENTED_EDGE ( 'NONE', *, *, #23501, .F. ) ;
#141654=FACE_OUTER_BOUND ( 'NONE', #233677, .T. ) ;
#141790=EDGE_LOOP ( 'NONE', ( #71948, #71945, #8058, #133403 ) ) ;
#141883=CARTESIAN_POINT ( 'NONE',  ( -16.77977881697927032, 22.98649307498303784, -230.9434316717720321 ) ) ;
#141900=EDGE_CURVE ( 'NONE', #196055, #140686, #90871, .T. ) ;
#141978=CARTESIAN_POINT ( 'NONE',  ( -16.92209698673482166, 23.03151742425346526, -230.9636950939940618 ) ) ;
#142005=CYLINDRICAL_SURFACE ( 'NONE', #150808, 0.9000000000000014655 ) ;
#142367=CARTESIAN_POINT ( 'NONE',  ( -17.04761207306819770, 23.01416701742251902, -230.8676723288925245 ) ) ;
#142403=ORIENTED_EDGE ( 'NONE', *, *, #111394, .F. ) ;
#142581=CARTESIAN_POINT ( 'NONE',  ( -16.92507428761701505, 23.03395201945197357, -230.9649992399934320 ) ) ;
#142590=ORIENTED_EDGE ( 'NONE', *, *, #50746, .F. ) ;
#142642=CARTESIAN_POINT ( 'NONE',  ( -16.87304349924914604, 30.24631159100806599, -234.8151387799927363 ) ) ;
#142675=B_SPLINE_CURVE_WITH_KNOTS ( 'NONE', 3,
 ( #44943, #120647, #101004, #180599, #12257, #107477, #68362, #9663, #33129, #151772, #187046, #127044, #129618, #128342, #168793, #150476, #108764, #70960, #229995, #51326, #149199, #8394, #73524, #50071, #188294, #30535 ),
 .UNSPECIFIED., .F., .F.,
 ( 4, 2, 2, 2, 2, 2, 2, 2, 2, 2, 2, 2, 4 ),
 ( 0.005476422646581333500, 0.006160811967703513220, 0.006845201288825692940, 0.007187395949386799279, 0.007529590609947904752, 0.007871785270509010224, 0.008213979931070116564, 0.008556174591631222903, 0.008898369252192329243, 0.009240563912753433848, 0.009582758573314538453, 0.01026714789443678583, 0.01095153721555903320 ),
 .UNSPECIFIED. ) ;
#142770=ORIENTED_EDGE ( 'NONE', *, *, #139451, .T. ) ;
#142779=VERTEX_POINT ( 'NONE', #19402 ) ;
#142816=CARTESIAN_POINT ( 'NONE',  ( -23.25000000000000355, 20.83093076766827423, -227.7429161672744442 ) ) ;
#142909=CARTESIAN_POINT ( 'NONE',  ( -18.37160782347004329, 20.70136879309603728, -227.9847839959967075 ) ) ;
#142914=DIRECTION ( 'NONE',  ( 1.186688945009009831E-16, -0.4721928772777346239, -0.8814952561688430555 ) ) ;
#143063=CARTESIAN_POINT ( 'NONE',  ( 13.99999999999999822, 26.54497872210689735, -232.9592037335782209 ) ) ;
#143064=LINE ( 'NONE', #238327, #227817 ) ;
#143313=CARTESIAN_POINT ( 'NONE',  ( 17.74533788810830615, 21.32866134633797017, -229.0662642334345378 ) ) ;
#143391=EDGE_CURVE ( 'NONE', #89902, #100947, #126308, .T. ) ;
#143479=EDGE_CURVE ( 'NONE', #102599, #137205, #68487, .T. ) ;
#143766=EDGE_CURVE ( 'NONE', #81187, #245289, #12984, .T. ) ;
#143781=DIRECTION ( 'NONE',  ( -1.073024830501117528E-15, -0.8814952561688430555, 0.4721928772777346239 ) ) ;
#143980=ORIENTED_EDGE ( 'NONE', *, *, #342, .T. ) ;
#144008=EDGE_LOOP ( 'NONE', ( #207600, #54522, #187463, #51375, #226411, #25755, #95026, #29052, #70592, #174561, #218109, #153888, #93722, #141631 ) ) ;
#144114=ORIENTED_EDGE ( 'NONE', *, *, #165875, .F. ) ;
#144157=EDGE_LOOP ( 'NONE', ( #24284, #142770 ) ) ;
#144199=CARTESIAN_POINT ( 'NONE',  ( -18.38639463286148867, 20.70353292814713342, -227.9807439630503154 ) ) ;
#144257=CARTESIAN_POINT ( 'NONE',  ( -16.84421487269768747, 22.99525848796287519, -230.9442721744328821 ) ) ;
#144260=DIRECTION ( 'NONE',  ( 1.000000000000000000, 0.000000000000000000, 0.000000000000000000 ) ) ;
#144400=DIRECTION ( 'NONE',  ( 1.073024830501117528E-15, -0.8814952561688430555, 0.4721928772777346239 ) ) ;
#144486=LINE ( 'NONE', #224034, #168231 ) ;
#144737=ORIENTED_EDGE ( 'NONE', *, *, #227232, .T. ) ;
#144807=DIRECTION ( 'NONE',  ( 0.000000000000000000, 0.8814952561688430555, -0.4721928772777346239 ) ) ;
#144885=ORIENTED_EDGE ( 'NONE', *, *, #231093, .F. ) ;
#144947=CARTESIAN_POINT ( 'NONE',  ( -16.77732147262506146, 30.19251626946681810, -234.8042213958585478 ) ) ;
#145045=CARTESIAN_POINT ( 'NONE',  ( -16.85312841634288006, 23.17876450014587419, -231.0838577861638896 ) ) ;
#145210=VECTOR ( 'NONE', #119224, 1000.000000000000000 ) ;
#145412=LINE ( 'NONE', #223655, #76464 ) ;
#145493=CARTESIAN_POINT ( 'NONE',  ( 15.74999999999999645, 26.30888228346803714, -233.3999513616626587 ) ) ;
#145509=CARTESIAN_POINT ( 'NONE',  ( -16.94165728009537375, 30.26040018438209955, -234.7930488771960427 ) ) ;
#145584=CARTESIAN_POINT ( 'NONE',  ( 18.54999999999999716, 29.63969710739366903, -235.8648393122026334 ) ) ;
#146069=LINE ( 'NONE', #161822, #198093 ) ;
#146082=VECTOR ( 'NONE', #216824, 1000.000000000000000 ) ;
#146089=FACE_OUTER_BOUND ( 'NONE', #222506, .T. ) ;
#146247=VERTEX_POINT ( 'NONE', #82297 ) ;
#146326=CARTESIAN_POINT ( 'NONE',  ( -16.87372386987899020, 23.38540140777922716, -231.2319906532857203 ) ) ;
#146377=FACE_OUTER_BOUND ( 'NONE', #251092, .T. ) ;
#146459=CARTESIAN_POINT ( 'NONE',  ( -16.93353400591625757, 30.30500211285577450, -234.7979474545380754 ) ) ;
#146776=CARTESIAN_POINT ( 'NONE',  ( -16.93301857435210067, 30.25028764630435418, -234.8007464032908445 ) ) ;
#147300=LINE ( 'NONE', #127753, #174451 ) ;
#147349=ORIENTED_EDGE ( 'NONE', *, *, #23592, .F. ) ;
#147623=CARTESIAN_POINT ( 'NONE',  ( -16.79139129368507000, 22.99352567686698023, -230.9490794793520649 ) ) ;
#147668=VECTOR ( 'NONE', #117158, 1000.000000000000000 ) ;
#147696=CARTESIAN_POINT ( 'NONE',  ( 18.39999999999999503, 20.94763808724815846, -234.7254930126486556 ) ) ;
#147713=ORIENTED_EDGE ( 'NONE', *, *, #167151, .F. ) ;
#147774=CARTESIAN_POINT ( 'NONE',  ( -16.93344882324368683, 30.28388429518871305, -234.7957375116174035 ) ) ;
#147779=CARTESIAN_POINT ( 'NONE',  ( -16.89021194854739960, 30.11162787777481498, -234.7563164417510677 ) ) ;
#148221=B_SPLINE_CURVE_WITH_KNOTS ( 'NONE', 3,
 ( #135282, #64744, #240827, #139112, #222514, #218671, #84252, #124731, #144257, #81702 ),
 .UNSPECIFIED., .F., .F.,
 ( 4, 2, 2, 2, 4 ),
 ( 0.000000000000000000, 0.0003916577441626793482, 0.0005874866162440234947, 0.0006854010522846912040, 0.0007833154883253590217 ),
 .UNSPECIFIED. ) ;
#148444=AXIS2_PLACEMENT_3D ( 'NONE', #205654, #161433, #85682 ) ;
#148628=VECTOR ( 'NONE', #224680, 1000.000000000000000 ) ;
#149199=CARTESIAN_POINT ( 'NONE',  ( 15.15590539855245034, 25.17497023110846044, -232.7237055342689303 ) ) ;
#149269=EDGE_LOOP ( 'NONE', ( #196263, #172405, #115553, #206015 ) ) ;
#149325=CARTESIAN_POINT ( 'NONE',  ( -14.00000000000000178, 26.54497872210690090, -232.9592037335782209 ) ) ;
#149344=CARTESIAN_POINT ( 'NONE',  ( -18.40000000000000213, 30.85877660472528916, -233.5890472672530507 ) ) ;
#149578=DIRECTION ( 'NONE',  ( 0.000000000000000000, 0.8814952561688429444, -0.4721928772777345684 ) ) ;
#149654=FACE_OUTER_BOUND ( 'NONE', #44421, .T. ) ;
#149998=ORIENTED_EDGE ( 'NONE', *, *, #46136, .T. ) ;
#150451=ORIENTED_EDGE ( 'NONE', *, *, #252526, .T. ) ;
#150476=CARTESIAN_POINT ( 'NONE',  ( 14.45204356427542258, 24.86276468521554150, -232.5111033352153527 ) ) ;
#150479=DIRECTION ( 'NONE',  ( 0.000000000000000000, -0.4721928772777346239, -0.8814952561688430555 ) ) ;
#150506=ORIENTED_EDGE ( 'NONE', *, *, #254006, .T. ) ;
#150545=CARTESIAN_POINT ( 'NONE',  ( -12.60206096961791999, 25.37811339336344929, -232.8563427119264304 ) ) ;
#150563=CARTESIAN_POINT ( 'NONE',  ( -16.77683809663752257, 22.98839712131283974, -230.9453208111996503 ) ) ;
#150640=CARTESIAN_POINT ( 'NONE',  ( 12.48201962039796342, 27.09559348180859217, -233.7911270184620491 ) ) ;
#150737=CIRCLE ( 'NONE', #67346, 0.5000000000000004441 ) ;
#150763=ORIENTED_EDGE ( 'NONE', *, *, #110961, .F. ) ;
#150808=AXIS2_PLACEMENT_3D ( 'NONE', #42918, #25929, #183719 ) ;
#150839=CARTESIAN_POINT ( 'NONE',  ( -18.40000000000000213, 20.94763808724815846, -234.7254930126486556 ) ) ;
#150870=ADVANCED_FACE ( 'NONE', ( #249388 ), #220001, .T. ) ;
#150937=EDGE_CURVE ( 'NONE', #167521, #170251, #77232, .T. ) ;
#151051=DIRECTION ( 'NONE',  ( -0.000000000000000000, 0.8814952561688430555, -0.4721928772777346239 ) ) ;
#151180=EDGE_CURVE ( 'NONE', #60665, #97217, #130487, .T. ) ;
#151220=EDGE_CURVE ( 'NONE', #46929, #164364, #193052, .T. ) ;
#151272=ORIENTED_EDGE ( 'NONE', *, *, #184531, .T. ) ;
#151354=CARTESIAN_POINT ( 'NONE',  ( -15.75000000000000355, 26.54497872210690090, -232.9592037335782209 ) ) ;
#151362=LINE ( 'NONE', #191782, #192412 ) ;
#151402=DIRECTION ( 'NONE',  ( -1.020425574104003999E-15, 0.8814952561688429444, -0.4721928772777345684 ) ) ;
#151431=AXIS2_PLACEMENT_3D ( 'NONE', #79485, #200736, #177358 ) ;
#151655=CARTESIAN_POINT ( 'NONE',  ( -16.87333278164169670, 29.74859725134929889, -234.6383007634102000 ) ) ;
#151713=EDGE_CURVE ( 'NONE', #36696, #40232, #24065, .T. ) ;
#151772=CARTESIAN_POINT ( 'NONE',  ( 13.43443725621852636, 24.89114276590144570, -232.5309687781012826 ) ) ;
#151777=CARTESIAN_POINT ( 'NONE',  ( -16.87383368123029825, 22.97806745954241947, -230.9350634111226270 ) ) ;
#152021=LINE ( 'NONE', #112866, #157926 ) ;
#152038=CARTESIAN_POINT ( 'NONE',  ( -16.93226657140833069, 22.93862264524221573, -230.8577296051770418 ) ) ;
#152262=CARTESIAN_POINT ( 'NONE',  ( -17.22361732159831860, 31.52054061960090436, -235.0627536016827719 ) ) ;
#152390=LINE ( 'NONE', #154954, #33534 ) ;
#152402=ORIENTED_EDGE ( 'NONE', *, *, #185409, .T. ) ;
#152449=AXIS2_PLACEMENT_3D ( 'NONE', #218389, #136273, #176736 ) ;
#152550=CARTESIAN_POINT ( 'NONE',  ( -16.94445028196807002, 30.26380394232451465, -234.7901145182196956 ) ) ;
#152708=DIRECTION ( 'NONE',  ( -1.000000000000000000, -0.000000000000000000, -0.000000000000000000 ) ) ;
#152866=CARTESIAN_POINT ( 'NONE',  ( -16.87036670365548474, 30.33914847462230568, -234.8334748671511818 ) ) ;
#152944=CARTESIAN_POINT ( 'NONE',  ( -16.97683809663752186, 29.54312324717475136, -234.4517840742876729 ) ) ;
#153081=CARTESIAN_POINT ( 'NONE',  ( -16.88815647973234135, 22.97600747097644813, -230.9330153782701984 ) ) ;
#153149=CARTESIAN_POINT ( 'NONE',  ( -13.77178122865954002, 24.82620238936339874, -232.4854380501665787 ) ) ;
#153328=FACE_BOUND ( 'NONE', #144157, .T. ) ;
#153513=CARTESIAN_POINT ( 'NONE',  ( 0.000000000000000000, 0.000000000000000000, 0.000000000000000000 ) ) ;
#153851=CARTESIAN_POINT ( 'NONE',  ( -16.98495255085916611, 30.24612551772337810, -234.7653289254189417 ) ) ;
#153888=ORIENTED_EDGE ( 'NONE', *, *, #170689, .F. ) ;
#154042=CARTESIAN_POINT ( 'NONE',  ( 18.39999999999999503, 23.82801463864234037, -229.3483719500187306 ) ) ;
#154052=CIRCLE ( 'NONE', #199818, 1.749999999999999778 ) ;
#154120=EDGE_CURVE ( 'NONE', #164364, #236786, #150737, .T. ) ;
#154155=CARTESIAN_POINT ( 'NONE',  ( -16.91256925476569251, 30.32690185447398790, -234.8310981037861609 ) ) ;
#154346=LINE ( 'NONE', #33113, #146082 ) ;
#154430=CARTESIAN_POINT ( 'NONE',  ( -12.29659703204451482, 25.90497867185234071, -233.1769111789295437 ) ) ;
#154459=CARTESIAN_POINT ( 'NONE',  ( -16.89935556175777265, 23.40971485048315159, -231.1662851018464835 ) ) ;
#154531=PLANE ( 'NONE',  #45855 ) ;
#154578=PLANE ( 'NONE',  #2595 ) ;
#154775=EDGE_CURVE ( 'NONE', #155129, #84120, #203220, .T. ) ;
#154835=CARTESIAN_POINT ( 'NONE',  ( -16.86757978335471719, 22.93962380547342050, -230.8967158438207719 ) ) ;
#154954=CARTESIAN_POINT ( 'NONE',  ( -17.01825945287481545, 30.11817903451004952, -234.7598257170722889 ) ) ;
#154969=DIRECTION ( 'NONE',  ( 0.000000000000000000, 0.8814952561688429444, -0.4721928772777345684 ) ) ;
#155109=ORIENTED_EDGE ( 'NONE', *, *, #18514, .F. ) ;
#155129=VERTEX_POINT ( 'NONE', #22406 ) ;
#155137=LINE ( 'NONE', #234634, #224486 ) ;
#155153=CARTESIAN_POINT ( 'NONE',  ( 15.74999999999999645, 26.30888228346803714, -233.3999513616626587 ) ) ;
#155316=ORIENTED_EDGE ( 'NONE', *, *, #54675, .F. ) ;
#155437=CARTESIAN_POINT ( 'NONE',  ( -18.37013991200266005, 33.97311679673139651, -235.0667207747197267 ) ) ;
#155891=CARTESIAN_POINT ( 'NONE',  ( -16.80117486205003630, 30.20515730058129833, -234.8068064003087159 ) ) ;
#156025=VERTEX_POINT ( 'NONE', #42615 ) ;
#156124=CARTESIAN_POINT ( 'NONE',  ( -16.86337532320261801, 22.90501630980172720, -230.8619360331160237 ) ) ;
#156305=ORIENTED_EDGE ( 'NONE', *, *, #50157, .F. ) ;
#156468=DIRECTION ( 'NONE',  ( 1.000000000000000000, 0.000000000000000000, 0.000000000000000000 ) ) ;
#156847=VECTOR ( 'NONE', #138605, 1000.000000000000000 ) ;
#157142=EDGE_LOOP ( 'NONE', ( #127620, #17649, #144114, #923 ) ) ;
#157326=EDGE_LOOP ( 'NONE', ( #120689, #87961, #224048, #82341 ) ) ;
#157361=DIRECTION ( 'NONE',  ( 0.000000000000000000, 0.8814952561688430555, -0.4721928772777346239 ) ) ;
#157400=ORIENTED_EDGE ( 'NONE', *, *, #195676, .T. ) ;
#157501=AXIS2_PLACEMENT_3D ( 'NONE', #132321, #210582, #211884 ) ;
#157594=ORIENTED_EDGE ( 'NONE', *, *, #73368, .F. ) ;
#157716=CARTESIAN_POINT ( 'NONE',  ( -16.27683809663751191, 22.60660220755888972, -231.4167412770961505 ) ) ;
#157777=CARTESIAN_POINT ( 'NONE',  ( 18.39999999999999503, 28.17589918783267322, -238.5974746063260739 ) ) ;
#157860=DIRECTION ( 'NONE',  ( 1.186688945009009831E-16, -0.4721928772777346239, -0.8814952561688430555 ) ) ;
#157926=VECTOR ( 'NONE', #249813, 1000.000000000000000 ) ;
#157989=PLANE ( 'NONE',  #198808 ) ;
#158227=AXIS2_PLACEMENT_3D ( 'NONE', #143063, #122242, #182219 ) ;
#159180=EDGE_CURVE ( 'NONE', #249547, #239889, #249675, .T. ) ;
#159478=EDGE_CURVE ( 'NONE', #239027, #112332, #124788, .T. ) ;
#160029=CARTESIAN_POINT ( 'NONE',  ( -18.40000000000000213, 28.17589918783267322, -238.5974746063260739 ) ) ;
#160121=EDGE_CURVE ( 'NONE', #13346, #156025, #194895, .T. ) ;
#160316=CARTESIAN_POINT ( 'NONE',  ( -18.40000000000000213, 23.66078093222370882, -229.5728445495489893 ) ) ;
#160389=LINE ( 'NONE', #59951, #129722 ) ;
#160651=LINE ( 'NONE', #124076, #43981 ) ;
#161072=ORIENTED_EDGE ( 'NONE', *, *, #170227, .F. ) ;
#161189=CARTESIAN_POINT ( 'NONE',  ( -14.45422546970484667, 27.84954713259351777, -234.1111166998237536 ) ) ;
#161191=EDGE_CURVE ( 'NONE', #239027, #109775, #3746, .T. ) ;
#161282=VECTOR ( 'NONE', #234548, 1000.000000000000000 ) ;
#161433=DIRECTION ( 'NONE',  ( 1.186688945009009584E-16, -0.4721928772777346239, -0.8814952561688430555 ) ) ;
#161822=CARTESIAN_POINT ( 'NONE',  ( -18.40000000000000213, 19.44861527341281615, -230.3234391047226666 ) ) ;
#161860=EDGE_CURVE ( 'NONE', #205806, #156025, #32583, .T. ) ;
#161965=CARTESIAN_POINT ( 'NONE',  ( 20.09999999999999787, 19.88654501311280498, -229.5059066796121101 ) ) ;
#162069=ORIENTED_EDGE ( 'NONE', *, *, #128636, .T. ) ;
#162074=DIRECTION ( 'NONE',  ( 1.000000000000000000, 0.000000000000000000, 0.000000000000000000 ) ) ;
#162232=ORIENTED_EDGE ( 'NONE', *, *, #118401, .T. ) ;
#162238=ORIENTED_EDGE ( 'NONE', *, *, #196703, .T. ) ;
#162523=CARTESIAN_POINT ( 'NONE',  ( -18.35235881385853318, 20.70033119311990077, -227.9867209999219426 ) ) ;
#162605=ADVANCED_FACE ( 'NONE', ( #189234 ), #170998, .F. ) ;
#162631=CARTESIAN_POINT ( 'NONE',  ( -17.22767730081888971, 22.02731797329168018, -229.9728559097052312 ) ) ;
#163352=CARTESIAN_POINT ( 'NONE',  ( -21.65000000000000213, 21.70314669089253812, -233.3151006027785286 ) ) ;
#163659=EDGE_CURVE ( 'NONE', #128551, #42653, #142675, .T. ) ;
#163758=CARTESIAN_POINT ( 'NONE',  ( -12.33960340485503693, 26.81162386565848621, -233.6570620184931215 ) ) ;
#163796=CARTESIAN_POINT ( 'NONE',  ( 15.39170923737819585, 27.26819834643092477, -233.8689871410715853 ) ) ;
#164364=VERTEX_POINT ( 'NONE', #171687 ) ;
#164372=CARTESIAN_POINT ( 'NONE',  ( -16.89268316805466341, 22.97380970494227626, -230.9308293615217451 ) ) ;
#164452=LINE ( 'NONE', #224403, #40379 ) ;
#164548=ORIENTED_EDGE ( 'NONE', *, *, #250664, .T. ) ;
#164554=AXIS2_PLACEMENT_3D ( 'NONE', #184830, #144400, #123587 ) ;
#164605=ORIENTED_EDGE ( 'NONE', *, *, #240103, .T. ) ;
#164628=CARTESIAN_POINT ( 'NONE',  ( -16.85939591225058720, 23.23024940989758136, -231.1209430754783796 ) ) ;
#164713=B_SPLINE_CURVE_WITH_KNOTS ( 'NONE', 3,
 ( #43807, #223701, #102452, #119499, #163758, #243268, #123345, #202866, #45084, #4651, #60781, #3369, #24260, #25534, #241997, #161189, #787, #105006, #122061, #21680, #199028, #219863, #180752, #85455, #141612, #103740, #184588, #240723, #221139, #5931 ),
 .UNSPECIFIED., .F., .F.,
 ( 4, 2, 2, 2, 2, 2, 2, 2, 2, 2, 2, 2, 2, 2, 4 ),
 ( 3.469446951953614189E-18, 0.0003422764154113311212, 0.0006845528308226587729, 0.001026829246233986479, 0.001369105661645314076, 0.002053658492467989004, 0.002738211323290663714, 0.003080487738701998685, 0.003422764154113333221, 0.003765040569524669058, 0.004107316984936004028, 0.004449593400347338565, 0.004791869815758673101, 0.005134146231170011974, 0.005476422646581350848 ),
 .UNSPECIFIED. ) ;
#164766=CARTESIAN_POINT ( 'NONE',  ( -16.85312964099708921, 29.97125116805203859, -234.7224086421056199 ) ) ;
#164876=DIRECTION ( 'NONE',  ( -1.000000000000000000, 0.000000000000000000, 0.000000000000000000 ) ) ;
#165004=EDGE_CURVE ( 'NONE', #171663, #42537, #151362, .T. ) ;
#165236=DIRECTION ( 'NONE',  ( -1.000000000000000000, 0.000000000000000000, 0.000000000000000000 ) ) ;
#165356=CARTESIAN_POINT ( 'NONE',  ( -16.87036670365549895, 22.88247411645692253, -230.8391385443351282 ) ) ;
#165703=ORIENTED_EDGE ( 'NONE', *, *, #104116, .T. ) ;
#165875=EDGE_CURVE ( 'NONE', #219246, #146247, #32759, .T. ) ;
#165930=CARTESIAN_POINT ( 'NONE',  ( -16.81453046979150301, 23.02733327219609905, -230.9738165231199218 ) ) ;
#166005=CARTESIAN_POINT ( 'NONE',  ( -17.11825945287481332, 30.25354784785470486, -234.7188954791831748 ) ) ;
#166040=FACE_OUTER_BOUND ( 'NONE', #103353, .T. ) ;
#166076=CARTESIAN_POINT ( 'NONE',  ( -16.94107738177414291, 30.32481141862675145, -234.7976376674202186 ) ) ;
#166102=ORIENTED_EDGE ( 'NONE', *, *, #255365, .T. ) ;
#166190=CARTESIAN_POINT ( 'NONE',  ( -17.11825945287481332, 30.16539832223782369, -234.6716761914553899 ) ) ;
#166194=DIRECTION ( 'NONE',  ( 0.000000000000000000, -0.8814952561688429444, 0.4721928772777345684 ) ) ;
#166258=AXIS2_PLACEMENT_3D ( 'NONE', #116621, #198719, #140010 ) ;
#166513=VERTEX_POINT ( 'NONE', #22324 ) ;
#166553=CARTESIAN_POINT ( 'NONE',  ( 20.73486653747088937, 21.93924312953142319, -232.8743529746940624 ) ) ;
#166624=CARTESIAN_POINT ( 'NONE',  ( 16.27683809663749770, 19.69766786220171539, -229.8585047820796490 ) ) ;
#166954=ORIENTED_EDGE ( 'NONE', *, *, #111394, .T. ) ;
#166974=ORIENTED_EDGE ( 'NONE', *, *, #257181, .T. ) ;
#166988=EDGE_CURVE ( 'NONE', #89559, #108947, #183422, .T. ) ;
#167151=EDGE_CURVE ( 'NONE', #167521, #117799, #252578, .T. ) ;
#167347=ORIENTED_EDGE ( 'NONE', *, *, #92104, .T. ) ;
#167434=ADVANCED_FACE ( 'NONE', ( #63357 ), #182045, .F. ) ;
#167521=VERTEX_POINT ( 'NONE', #250978 ) ;
#167788=UNCERTAINTY_MEASURE_WITH_UNIT (LENGTH_MEASURE( 1.000000000000000082E-05 ), #231420, 'distance_accuracy_value', 'NONE');
#167794=CARTESIAN_POINT ( 'NONE',  ( -23.25000000000000355, 34.05335961020092128, -234.8258093264404351 ) ) ;
#167814=VECTOR ( 'NONE', #57060, 1000.000000000000114 ) ;
#167845=VERTEX_POINT ( 'NONE', #69198 ) ;
#168048=ORIENTED_EDGE ( 'NONE', *, *, #134514, .T. ) ;
#168133=EDGE_LOOP ( 'NONE', ( #224625, #232521, #92144, #120508, #201986 ) ) ;
#168217=ORIENTED_EDGE ( 'NONE', *, *, #93471, .F. ) ;
#168231=VECTOR ( 'NONE', #85781, 1000.000000000000000 ) ;
#168467=CARTESIAN_POINT ( 'NONE',  ( 18.39999999999999503, 23.69729366125098835, -229.5924034189314682 ) ) ;
#168572=ORIENTED_EDGE ( 'NONE', *, *, #150937, .T. ) ;
#168660=ORIENTED_EDGE ( 'NONE', *, *, #84753, .T. ) ;
#168793=CARTESIAN_POINT ( 'NONE',  ( 14.22821877134046353, 24.82620238936339874, -232.4854380501665787 ) ) ;
#168854=DIRECTION ( 'NONE',  ( 0.000000000000000000, 0.8814952561688428334, -0.4721928772777349015 ) ) ;
#169200=ORIENTED_EDGE ( 'NONE', *, *, #172983, .T. ) ;
#169416=DIRECTION ( 'NONE',  ( 1.000000000000000000, 0.000000000000000000, 0.000000000000000000 ) ) ;
#169524=DIRECTION ( 'NONE',  ( 1.000000000000000000, 0.000000000000000000, 0.000000000000000000 ) ) ;
#169622=EDGE_CURVE ( 'NONE', #89559, #5154, #145412, .T. ) ;
#169662=VECTOR ( 'NONE', #132712, 1000.000000000000000 ) ;
#169739=ORIENTED_EDGE ( 'NONE', *, *, #167151, .T. ) ;
#169950=CARTESIAN_POINT ( 'NONE',  ( -16.80070461187955999, 30.20900493031334477, -234.8084786630442977 ) ) ;
#170076=CARTESIAN_POINT ( 'NONE',  ( 18.39999999999999147, 19.44861527341281615, -230.3234391047226666 ) ) ;
#170170=CARTESIAN_POINT ( 'NONE',  ( -16.78569801330232991, 22.98318547630623954, -230.9401490402474622 ) ) ;
#170227=EDGE_CURVE ( 'NONE', #89902, #81187, #190700, .T. ) ;
#170251=VERTEX_POINT ( 'NONE', #206385 ) ;
#170255=CARTESIAN_POINT ( 'NONE',  ( 13.54577453029515866, 27.84954713259350711, -234.1111166998236683 ) ) ;
#170325=ADVANCED_FACE ( 'NONE', ( #74615 ), #5176, .T. ) ;
#170657=CARTESIAN_POINT ( 'NONE',  ( -20.65000000000000568, 17.95055421627409231, -233.1200372299043693 ) ) ;
#170689=EDGE_CURVE ( 'NONE', #295, #56834, #114448, .T. ) ;
#170998=PLANE ( 'NONE',  #3875 ) ;
#171000=CARTESIAN_POINT ( 'NONE',  ( -17.11825945287482753, 23.02528674727019364, -230.8469138855057281 ) ) ;
#171011=CARTESIAN_POINT ( 'NONE',  ( -21.65000000000000213, 21.70314669089253812, -233.3151006027785286 ) ) ;
#171235=CARTESIAN_POINT ( 'NONE',  ( -16.83233564386400616, 30.08637999345557290, -234.7652289483340269 ) ) ;
#171364=CARTESIAN_POINT ( 'NONE',  ( -16.88560720703333473, 22.97666984193590167, -230.9336739665168921 ) ) ;
#171497=EDGE_CURVE ( 'NONE', #164364, #56834, #34237, .T. ) ;
#171663=VERTEX_POINT ( 'NONE', #103146 ) ;
#171687=CARTESIAN_POINT ( 'NONE',  ( 21.13736287352038445, 22.07931554675867858, -232.6128641271329229 ) ) ;
#171809=CIRCLE ( 'NONE', #50943, 1.749999999999999778 ) ;
#171973=EDGE_CURVE ( 'NONE', #236786, #295, #216383, .T. ) ;
#171979=ORIENTED_EDGE ( 'NONE', *, *, #233220, .F. ) ;
#171984=CARTESIAN_POINT ( 'NONE',  ( -17.11825945287482753, 23.11343627288707481, -230.8941331732335129 ) ) ;
#171994=CIRCLE ( 'NONE', #59477, 14.30833333333334956 ) ;
#172341=DIRECTION ( 'NONE',  ( -1.000000000000000000, 0.000000000000000000, 0.000000000000000000 ) ) ;
#172361=DIRECTION ( 'NONE',  ( 0.000000000000000000, 0.4721928772777345129, 0.8814952561688430555 ) ) ;
#172405=ORIENTED_EDGE ( 'NONE', *, *, #73337, .T. ) ;
#172443=CARTESIAN_POINT ( 'NONE',  ( -18.40000000000000213, 33.92901942162173157, -235.0579290632217067 ) ) ;
#172519=CARTESIAN_POINT ( 'NONE',  ( -16.83794479845802172, 30.05980643715662382, -234.7553781105508790 ) ) ;
#172524=CARTESIAN_POINT ( 'NONE',  ( -16.88705144915422096, 29.95864726180315429, -234.6743689137096567 ) ) ;
#172585=VECTOR ( 'NONE', #249373, 1000.000000000000000 ) ;
#172816=CARTESIAN_POINT ( 'NONE',  ( 12.60873083341397027, 27.26868795068922680, -233.8692014934036081 ) ) ;
#172983=EDGE_CURVE ( 'NONE', #113, #155129, #257996, .T. ) ;
#173293=VECTOR ( 'NONE', #18155, 999.9999999999998863 ) ;
#173445=VERTEX_POINT ( 'NONE', #45112 ) ;
#173530=CARTESIAN_POINT ( 'NONE',  ( -17.11825945287481687, 30.25354784785470841, -234.7188954791831748 ) ) ;
#173571=LINE ( 'NONE', #53571, #124890 ) ;
#173688=DIRECTION ( 'NONE',  ( -1.073024830501117528E-15, 0.8814952561688430555, -0.4721928772777346239 ) ) ;
#173721=EDGE_CURVE ( 'NONE', #113, #84120, #164452, .T. ) ;
#173807=FACE_OUTER_BOUND ( 'NONE', #65740, .T. ) ;
#173812=CARTESIAN_POINT ( 'NONE',  ( -16.87683809663752399, 29.62235354460948500, -234.5896431630760617 ) ) ;
#174373=LINE ( 'NONE', #253843, #41840 ) ;
#174447=DIRECTION ( 'NONE',  ( 1.020425574104003999E-15, 0.8814952561688430555, -0.4721928772777346239 ) ) ;
#174451=VECTOR ( 'NONE', #46900, 1000.000000000000000 ) ;
#174561=ORIENTED_EDGE ( 'NONE', *, *, #115041, .F. ) ;
#174573=ORIENTED_EDGE ( 'NONE', *, *, #252526, .F. ) ;
#175019=CARTESIAN_POINT ( 'NONE',  ( -18.40000000000000213, 33.85569253519368260, -235.0339796035492554 ) ) ;
#175086=CARTESIAN_POINT ( 'NONE',  ( -16.93710578446422588, 29.96937912356857225, -234.6801176782661571 ) ) ;
#175303=CARTESIAN_POINT ( 'NONE',  ( -16.87683809663752399, 23.59405348476696318, -231.3784738672519836 ) ) ;
#175596=CARTESIAN_POINT ( 'NONE',  ( -18.35668295345803713, 33.92263863280957281, -235.0698407953532296 ) ) ;
#175762=CARTESIAN_POINT ( 'NONE',  ( -16.92507428761700083, 30.15044400021737658, -234.7771091759292688 ) ) ;
#175925=DIRECTION ( 'NONE',  ( 1.000000000000000000, 0.000000000000000000, 0.000000000000000000 ) ) ;
#176073=CARTESIAN_POINT ( 'NONE',  ( -16.93388492042257454, 30.26908302050733823, -234.7969376182378198 ) ) ;
#176269=CARTESIAN_POINT ( 'NONE',  ( -18.41431012584570226, 33.94987820762823816, -235.0681983671880175 ) ) ;
#176275=PLANE ( 'NONE',  #128831 ) ;
#176587=( NAMED_UNIT ( * ) PLANE_ANGLE_UNIT ( ) SI_UNIT ( $, .RADIAN. ) );
#176736=DIRECTION ( 'NONE',  ( 0.000000000000000000, 0.7116622890665382783, 0.7025217336998015316 ) ) ;
#176817=ORIENTED_EDGE ( 'NONE', *, *, #4404, .T. ) ;
#176836=VERTEX_POINT ( 'NONE', #69190 ) ;
#177107=CARTESIAN_POINT ( 'NONE',  ( -18.39999999999999858, 20.74413403641815989, -228.0104766523929243 ) ) ;
#177163=LINE ( 'NONE', #217519, #59210 ) ;
#177214=LINE ( 'NONE', #138033, #54538 ) ;
#177235=CARTESIAN_POINT ( 'NONE',  ( -20.65000000000000568, 28.93140779147704933, -237.1870821964559184 ) ) ;
#177322=EDGE_CURVE ( 'NONE', #108947, #41838, #11825, .T. ) ;
#177358=DIRECTION ( 'NONE',  ( -1.000000000000000000, -7.709882115452463178E-15, 0.000000000000000000 ) ) ;
#177415=CARTESIAN_POINT ( 'NONE',  ( -17.27223548802031061, 22.03327853370796419, -229.9804127912456693 ) ) ;
#177976=EDGE_CURVE ( 'NONE', #56834, #195949, #4398, .T. ) ;
#178015=CARTESIAN_POINT ( 'NONE',  ( -16.78805706634180339, 30.20034948041843492, -234.8058246103456383 ) ) ;
#178218=VERTEX_POINT ( 'NONE', #19838 ) ;
#178232=VECTOR ( 'NONE', #150479, 1000.000000000000000 ) ;
#178270=ORIENTED_EDGE ( 'NONE', *, *, #211636, .F. ) ;
#178310=PLANE ( 'NONE',  #55228 ) ;
#178358=CARTESIAN_POINT ( 'NONE',  ( -21.65000000000000213, 30.11817903451004952, -234.7598257170722889 ) ) ;
#178586=CARTESIAN_POINT ( 'NONE',  ( -16.94445028196807002, 30.26380394232451465, -234.7901145182196956 ) ) ;
#178596=CARTESIAN_POINT ( 'NONE',  ( -18.40000000000000213, 23.66963324290564685, -229.6440402155210734 ) ) ;
#178704=CARTESIAN_POINT ( 'NONE',  ( -18.37013991200266005, 20.67483879484485954, -227.9431972973032998 ) ) ;
#178798=AXIS2_PLACEMENT_3D ( 'NONE', #232344, #173688, #190649 ) ;
#179071=PRESENTATION_STYLE_ASSIGNMENT (( #180325 ) ) ;
#179153=CARTESIAN_POINT ( 'NONE',  ( -16.82055514392384765, 23.00168983512579146, -230.9477172710467414 ) ) ;
#179378=CARTESIAN_POINT ( 'NONE',  ( -21.65000000000000213, 22.97806745954241947, -230.9350634111226270 ) ) ;
#179507=EDGE_CURVE ( 'NONE', #178218, #18361, #82370, .T. ) ;
#179527=CARTESIAN_POINT ( 'NONE',  ( -16.88495309932522304, 22.96663205285974385, -230.9236886748582549 ) ) ;
#179659=DIRECTION ( 'NONE',  ( 0.000000000000000000, 0.4721928772777346239, 0.8814952561688430555 ) ) ;
#179750=EDGE_LOOP ( 'NONE', ( #52599, #68309, #123601, #120139, #186610 ) ) ;
#179930=CARTESIAN_POINT ( 'NONE',  ( 13.99999999999999822, 26.54497872210689735, -232.9592037335782209 ) ) ;
#180134=VECTOR ( 'NONE', #174447, 1000.000000000000000 ) ;
#180147=EDGE_LOOP ( 'NONE', ( #74240, #136314, #184173, #219057, #250071 ) ) ;
#180233=EDGE_CURVE ( 'NONE', #112332, #220164, #124308, .T. ) ;
#180325=SURFACE_STYLE_USAGE ( .BOTH. , #1664 ) ;
#180599=CARTESIAN_POINT ( 'NONE',  ( 12.47034474403012716, 25.54511595760792630, -232.9618513057392875 ) ) ;
#180673=VECTOR ( 'NONE', #51136, 1000.000000000000000 ) ;
#180752=CARTESIAN_POINT ( 'NONE',  ( -15.39126916658603328, 27.26868795068923390, -233.8692014934036365 ) ) ;
#180821=VECTOR ( 'NONE', #86273, 1000.000000000000114 ) ;
#180951=CARTESIAN_POINT ( 'NONE',  ( -16.90202395485723486, 22.93886501610722917, -230.8959756691647272 ) ) ;
#181487=CARTESIAN_POINT ( 'NONE',  ( 23.24999999999999645, 20.94763808724816556, -234.7254930126486556 ) ) ;
#181760=CARTESIAN_POINT ( 'NONE',  ( -16.87683809663752399, 29.49590395944699139, -234.5399335999045718 ) ) ;
#181766=DIRECTION ( 'NONE',  ( -0.000000000000000000, 0.8814952561688430555, -0.4721928772777346239 ) ) ;
#182045=CYLINDRICAL_SURFACE ( 'NONE', #30357, 0.9000000000000014655 ) ;
#182219=DIRECTION ( 'NONE',  ( 1.000000000000000000, 5.603460673774838784E-17, 1.046060675573451523E-16 ) ) ;
#182434=CARTESIAN_POINT ( 'NONE',  ( -16.88853107394619357, 30.20933174956215694, -234.8076571479847985 ) ) ;
#182659=CARTESIAN_POINT ( 'NONE',  ( -16.93658623642890859, 22.95883090495301104, -230.8902928517333919 ) ) ;
#183216=CARTESIAN_POINT ( 'NONE',  ( -21.64999999999999858, 23.11343627288707481, -230.8941331732335129 ) ) ;
#183354=AXIS2_PLACEMENT_3D ( 'NONE', #217957, #39382, #139711 ) ;
#183358=CARTESIAN_POINT ( 'NONE',  ( 15.66039659514495064, 26.81162386565848621, -233.6570620184931215 ) ) ;
#183422=( BOUNDED_CURVE ( )  B_SPLINE_CURVE ( 3, ( #225299, #184913, #64957, #165356 ),
 .UNSPECIFIED., .F., .F. ) 
 B_SPLINE_CURVE_WITH_KNOTS ( ( 4, 4 ),
 ( 5.731445031868799056, 5.983100554402346560 ),
 .UNSPECIFIED. ) 
 CURVE ( )  GEOMETRIC_REPRESENTATION_ITEM ( )  RATIONAL_B_SPLINE_CURVE ( ( 1.000000000000000000, 0.9947294176030465618, 0.9947294176030465618, 1.000000000000000000 ) ) 
 REPRESENTATION_ITEM ( '' )  );
#183632=DIRECTION ( 'NONE',  ( 0.000000000000000000, -0.8814952561688429444, 0.4721928772777345684 ) ) ;
#183719=DIRECTION ( 'NONE',  ( -1.000000000000000000, 0.000000000000000000, 0.000000000000000000 ) ) ;
#183751=CARTESIAN_POINT ( 'NONE',  ( 20.05000000000002913, 21.70314669089255233, -233.3151006027785002 ) ) ;
#183953=DIRECTION ( 'NONE',  ( -1.000000000000000000, 0.000000000000000000, 0.000000000000000000 ) ) ;
#184147=EDGE_LOOP ( 'NONE', ( #104376, #36271 ) ) ;
#184173=ORIENTED_EDGE ( 'NONE', *, *, #16454, .T. ) ;
#184531=EDGE_CURVE ( 'NONE', #167845, #205806, #202525, .T. ) ;
#184588=CARTESIAN_POINT ( 'NONE',  ( -15.69373346032658745, 26.71301589465422666, -233.6087318245599533 ) ) ;
#184625=CARTESIAN_POINT ( 'NONE',  ( 14.22916352759893499, 27.90214353194706121, -234.1315669640962085 ) ) ;
#184803=VECTOR ( 'NONE', #31539, 1000.000000000000000 ) ;
#184830=CARTESIAN_POINT ( 'NONE',  ( 20.99999999999999645, 22.88362888408687468, -231.1113624623564249 ) ) ;
#184886=EDGE_LOOP ( 'NONE', ( #185192, #231014, #157594, #108657, #187170, #72790, #82602, #193865, #51806, #53698, #28668, #157400, #188366, #185729 ) ) ;
#184913=CARTESIAN_POINT ( 'NONE',  ( -17.71734398241074260, 21.30575908404109953, -229.0269313818040189 ) ) ;
#185192=ORIENTED_EDGE ( 'NONE', *, *, #62469, .F. ) ;
#185229=STYLED_ITEM ( 'NONE', ( #112745 ), #1633 ) ;
#185238=DIRECTION ( 'NONE',  ( 0.000000000000000000, -0.8814952561688430555, 0.4721928772777346239 ) ) ;
#185409=EDGE_CURVE ( 'NONE', #34727, #122206, #144486, .T. ) ;
#185526=VECTOR ( 'NONE', #219685, 1000.000000000000000 ) ;
#185555=ORIENTED_EDGE ( 'NONE', *, *, #100550, .F. ) ;
#185729=ORIENTED_EDGE ( 'NONE', *, *, #50157, .T. ) ;
#185914=PLANE ( 'NONE',  #74864 ) ;
#185975=ORIENTED_EDGE ( 'NONE', *, *, #42046, .F. ) ;
#186082=CARTESIAN_POINT ( 'NONE',  ( -16.89318236219976654, 22.97427065100864851, -230.9312879128452494 ) ) ;
#186495=ADVANCED_FACE ( 'NONE', ( #121180 ), #223741, .T. ) ;
#186610=ORIENTED_EDGE ( 'NONE', *, *, #18954, .F. ) ;
#186635=VECTOR ( 'NONE', #137232, 1000.000000000000000 ) ;
#186745=PRODUCT_DEFINITION_SHAPE ( 'NONE', 'NONE',  #195054 ) ;
#186813=CARTESIAN_POINT ( 'NONE',  ( -18.40000000000000213, 31.01370428745238783, -233.5116043003366713 ) ) ;
#186828=CARTESIAN_POINT ( 'NONE',  ( -15.55912972643740488, 29.60548742189585880, -236.1404802245173755 ) ) ;
#186917=CARTESIAN_POINT ( 'NONE',  ( -16.93826681692523195, 30.31948095044558045, -234.7979706876368766 ) ) ;
#187032=CARTESIAN_POINT ( 'NONE',  ( 18.39999999999999503, 31.17298305880675002, -240.2029303890703886 ) ) ;
#187046=CARTESIAN_POINT ( 'NONE',  ( 13.54556439290364267, 24.86329420051411532, -232.5114740807002818 ) ) ;
#187170=ORIENTED_EDGE ( 'NONE', *, *, #154120, .F. ) ;
#187305=CARTESIAN_POINT ( 'NONE',  ( -16.94180778212363236, 22.95772180291950448, -230.8760158671809393 ) ) ;
#187343=DIRECTION ( 'NONE',  ( 0.7071067811865795472, 0.3338907855511005218, 0.6233112732207110041 ) ) ;
#187463=ORIENTED_EDGE ( 'NONE', *, *, #170227, .T. ) ;
#188045=CARTESIAN_POINT ( 'NONE',  ( -16.80100426158792715, 23.00387470889453567, -230.9566579447254355 ) ) ;
#188184=CARTESIAN_POINT ( 'NONE',  ( -16.80100914604136264, 30.17404316570091538, -234.7975225174889999 ) ) ;
#188294=CARTESIAN_POINT ( 'NONE',  ( 15.75000000000000000, 26.10487691728826221, -233.2906712717672519 ) ) ;
#188330=ADVANCED_FACE ( 'NONE', ( #211991, #153328, #114150 ), #234094, .T. ) ;
#188366=ORIENTED_EDGE ( 'NONE', *, *, #143479, .F. ) ;
#188567=CARTESIAN_POINT ( 'NONE',  ( -16.93440969289731157, 22.94760179058243921, -230.8674840937281374 ) ) ;
#188646=EDGE_CURVE ( 'NONE', #192047, #97217, #113856, .T. ) ;
#189014=VERTEX_POINT ( 'NONE', #171011 ) ;
#189190=EDGE_CURVE ( 'NONE', #11282, #128551, #101653, .T. ) ;
#189234=FACE_OUTER_BOUND ( 'NONE', #140217, .T. ) ;
#189273=ORIENTED_EDGE ( 'NONE', *, *, #74095, .T. ) ;
#189353=EDGE_LOOP ( 'NONE', ( #161072, #97519, #62175 ) ) ;
#189374=CARTESIAN_POINT ( 'NONE',  ( -18.40000000000000213, 30.85877660472528916, -233.5890472672530507 ) ) ;
#189473=CARTESIAN_POINT ( 'NONE',  ( -16.97683810757273193, 29.66546359879749772, -234.5173184515128071 ) ) ;
#189489=CIRCLE ( 'NONE', #164554, 0.9000000000000014655 ) ;
#189938=DIRECTION ( 'NONE',  ( 1.186688945009010324E-16, -0.4721928772777346239, -0.8814952561688430555 ) ) ;
#190023=B_SPLINE_CURVE_WITH_KNOTS ( 'NONE', 3,
 ( #164372, #66553, #24880, #43142, #125241, #182659, #122692, #103079, #4000, #104363 ),
 .UNSPECIFIED., .F., .F.,
 ( 4, 3, 3, 4 ),
 ( 1.886897567106814762E-15, 3.877043166999436273E-05, 7.336897548476632052E-05, 7.659383120240038272E-05 ),
 .UNSPECIFIED. ) ;
#190178=LINE ( 'NONE', #170657, #53798 ) ;
#190226=CARTESIAN_POINT ( 'NONE',  ( 18.54999999999999716, 19.41435213583508812, -230.3874019357809289 ) ) ;
#190244=ORIENTED_EDGE ( 'NONE', *, *, #151180, .T. ) ;
#190649=DIRECTION ( 'NONE',  ( -1.000000000000000000, 0.000000000000000000, 0.000000000000000000 ) ) ;
#190700=LINE ( 'NONE', #10753, #172585 ) ;
#190874=ORIENTED_EDGE ( 'NONE', *, *, #71146, .F. ) ;
#190976=CARTESIAN_POINT ( 'NONE',  ( -12.25000000000000178, 26.30888228346803714, -233.3999513616626587 ) ) ;
#191297=DIRECTION ( 'NONE',  ( 1.186688945009009831E-16, -0.4721928772777346239, -0.8814952561688430555 ) ) ;
#191357=CARTESIAN_POINT ( 'NONE',  ( -16.94107738177414291, 30.32481141862674789, -234.7976376674202186 ) ) ;
#191423=LINE ( 'NONE', #94845, #180134 ) ;
#191462=CARTESIAN_POINT ( 'NONE',  ( 18.39999999999999503, 31.05627573922685514, -233.2203535436961488 ) ) ;
#191570=ORIENTED_EDGE ( 'NONE', *, *, #22855, .F. ) ;
#191573=AXIS2_PLACEMENT_3D ( 'NONE', #46183, #246949, #224815 ) ;
#191597=ADVANCED_FACE ( 'NONE', ( #203181 ), #221439, .F. ) ;
#191599=DIRECTION ( 'NONE',  ( -1.000000000000000000, 0.000000000000000000, 0.000000000000000000 ) ) ;
#191629=ORIENTED_EDGE ( 'NONE', *, *, #161191, .F. ) ;
#191731=ADVANCED_FACE ( 'NONE', ( #149654 ), #72225, .T. ) ;
#191782=CARTESIAN_POINT ( 'NONE',  ( -23.25000000000000355, 20.83093076766827423, -227.7429161672744442 ) ) ;
#191833=ORIENTED_EDGE ( 'NONE', *, *, #18960, .F. ) ;
#191991=EDGE_CURVE ( 'NONE', #140686, #89189, #164713, .T. ) ;
#192047=VERTEX_POINT ( 'NONE', #149344 ) ;
#192055=CARTESIAN_POINT ( 'NONE',  ( -16.77308656112213825, 30.20615826255785663, -234.8069537810542613 ) ) ;
#192233=DIRECTION ( 'NONE',  ( -0.000000000000000000, 0.8814952561688430555, -0.4721928772777346239 ) ) ;
#192337=CARTESIAN_POINT ( 'NONE',  ( 12.84435279558019616, 27.50042447306175220, -233.9693577020172199 ) ) ;
#192343=CARTESIAN_POINT ( 'NONE',  ( -18.39999999999999858, 20.76715588789282307, -228.0228088279911560 ) ) ;
#192412=VECTOR ( 'NONE', #14426, 1000.000000000000000 ) ;
#192593=ORIENTED_EDGE ( 'NONE', *, *, #184531, .F. ) ;
#192738=DIRECTION ( 'NONE',  ( -1.000000000000000000, -3.469446951953635015E-14, 0.000000000000000000 ) ) ;
#192859=AXIS2_PLACEMENT_3D ( 'NONE', #13496, #232560, #229962 ) ;
#192951=DIRECTION ( 'NONE',  ( 0.000000000000000000, -0.4721928772777346239, -0.8814952561688430555 ) ) ;
#193052=LINE ( 'NONE', #75679, #28704 ) ;
#193246=CARTESIAN_POINT ( 'NONE',  ( -17.29838795456134193, 31.51142988880226170, -235.0279307012797005 ) ) ;
#193327=CARTESIAN_POINT ( 'NONE',  ( -16.82542659449991262, 30.11558868677414225, -234.7760220207075861 ) ) ;
#193368=CARTESIAN_POINT ( 'NONE',  ( -17.78043020864321022, 32.67194018624805096, -235.1027381854017335 ) ) ;
#193748=DIRECTION ( 'NONE',  ( 1.000000000000000000, 0.000000000000000000, 0.000000000000000000 ) ) ;
#193865=ORIENTED_EDGE ( 'NONE', *, *, #46136, .F. ) ;
#194032=AXIS2_PLACEMENT_3D ( 'NONE', #31152, #105472, #46800 ) ;
#194058=LINE ( 'NONE', #256508, #167814 ) ;
#194558=CARTESIAN_POINT ( 'NONE',  ( -20.65000000000000568, 18.70606281991846842, -231.7096448200342138 ) ) ;
#194626=DIRECTION ( 'NONE',  ( -1.020425574104003999E-15, -0.8814952561688429444, 0.4721928772777345684 ) ) ;
#194631=CARTESIAN_POINT ( 'NONE',  ( -16.92280123533722147, 30.02947212702651925, -234.7123078551372259 ) ) ;
#194857=CARTESIAN_POINT ( 'NONE',  ( -16.87998658237769334, 23.16638972503378469, -231.0359424933138541 ) ) ;
#194895=CIRCLE ( 'NONE', #157501, 14.20833333333335347 ) ;
#194968=LINE ( 'NONE', #16331, #23593 ) ;
#195054=PRODUCT_DEFINITION ( 'UNKNOWN', '', #236198, #113224 ) ;
#195174=CARTESIAN_POINT ( 'NONE',  ( -18.39418127959864435, 33.92771173063928103, -235.0603702762365970 ) ) ;
#195311=ORIENTED_EDGE ( 'NONE', *, *, #14382, .F. ) ;
#195334=CARTESIAN_POINT ( 'NONE',  ( -17.11825945287481332, 30.11817903451004952, -234.7598257170722889 ) ) ;
#195491=CARTESIAN_POINT ( 'NONE',  ( -23.25000000000000355, 23.11343627288707481, -230.8941331732335129 ) ) ;
#195676=EDGE_CURVE ( 'NONE', #243571, #137205, #17312, .T. ) ;
#195939=CARTESIAN_POINT ( 'NONE',  ( -17.29158576265543346, 31.48883999867549477, -235.0235465672944031 ) ) ;
#195949=VERTEX_POINT ( 'NONE', #15393 ) ;
#195984=DIRECTION ( 'NONE',  ( 0.000000000000000000, 0.4721928772777346239, 0.8814952561688430555 ) ) ;
#196055=VERTEX_POINT ( 'NONE', #235697 ) ;
#196099=CARTESIAN_POINT ( 'NONE',  ( -21.65000000000000213, 28.93140779147704933, -237.1870821964559184 ) ) ;
#196263=ORIENTED_EDGE ( 'NONE', *, *, #143766, .F. ) ;
#196386=ORIENTED_EDGE ( 'NONE', *, *, #108846, .F. ) ;
#196664=LINE ( 'NONE', #218788, #137799 ) ;
#196703=EDGE_CURVE ( 'NONE', #220164, #136504, #234535, .T. ) ;
#196803=VECTOR ( 'NONE', #197391, 1000.000000000000114 ) ;
#196815=CARTESIAN_POINT ( 'NONE',  ( -16.87242674293850797, 22.97710641253713959, -230.9345486045511109 ) ) ;
#197022=ORIENTED_EDGE ( 'NONE', *, *, #62469, .T. ) ;
#197148=CARTESIAN_POINT ( 'NONE',  ( -16.93860193097148326, 30.27088047374820334, -234.7927206923158963 ) ) ;
#197204=CARTESIAN_POINT ( 'NONE',  ( 18.54999999999999716, 22.41143600680915782, -231.9928577185252152 ) ) ;
#197205=( BOUNDED_CURVE ( )  B_SPLINE_CURVE ( 3, ( #60260, #142367, #141101, #100645 ),
 .UNSPECIFIED., .F., .F. ) 
 B_SPLINE_CURVE_WITH_KNOTS ( ( 4, 4 ),
 ( 4.712388980384687898, 5.672655318024669491 ),
 .UNSPECIFIED. ) 
 CURVE ( )  GEOMETRIC_REPRESENTATION_ITEM ( )  RATIONAL_B_SPLINE_CURVE ( ( 1.000000000000000000, 0.9246222802177384015, 0.9246222802177384015, 1.000000000000000000 ) ) 
 REPRESENTATION_ITEM ( '' )  );
#197303=( NAMED_UNIT ( * ) PLANE_ANGLE_UNIT ( ) SI_UNIT ( $, .RADIAN. ) );
#197369=AXIS2_PLACEMENT_3D ( 'NONE', #70624, #229670, #92707 ) ;
#197391=DIRECTION ( 'NONE',  ( 0.7071067811865456854, -0.3338907855510742650, -0.6233112732207634066 ) ) ;
#197430=PLANE ( 'NONE',  #166258 ) ;
#197461=CARTESIAN_POINT ( 'NONE',  ( 20.27550659511088682, 19.63441466210375808, -229.9765866052221099 ) ) ;
#197462=ORIENTED_EDGE ( 'NONE', *, *, #163659, .F. ) ;
#197714=ORIENTED_EDGE ( 'NONE', *, *, #6954, .T. ) ;
#197770=CARTESIAN_POINT ( 'NONE',  ( 21.72449340488910252, 23.13575923509592513, -230.6406825367463966 ) ) ;
#198083=LINE ( 'NONE', #215081, #245084 ) ;
#198093=VECTOR ( 'NONE', #125240, 1000.000000000000000 ) ;
#198109=CIRCLE ( 'NONE', #85634, 1.749999999999998002 ) ;
#198125=CARTESIAN_POINT ( 'NONE',  ( -18.40000000000000213, 23.60914413563410008, -229.5451841312037402 ) ) ;
#198154=ORIENTED_EDGE ( 'NONE', *, *, #58298, .T. ) ;
#198156=LINE ( 'NONE', #19538, #21630 ) ;
#198170=DIRECTION ( 'NONE',  ( 0.5932847527679310229, -0.3801118060259202069, -0.7095972217059536291 ) ) ;
#198184=ADVANCED_FACE ( 'NONE', ( #256766 ), #78169, .F. ) ;
#198223=FACE_OUTER_BOUND ( 'NONE', #115665, .T. ) ;
#198260=CARTESIAN_POINT ( 'NONE',  ( 20.05000000000002913, 18.70606281991848263, -231.7096448200342138 ) ) ;
#198524=CARTESIAN_POINT ( 'NONE',  ( 18.54999999999999716, 29.63969710739366903, -235.8648393122026334 ) ) ;
#198719=DIRECTION ( 'NONE',  ( 1.000000000000000000, 8.995003028460479049E-16, -4.818376878839538654E-16 ) ) ;
#198808=AXIS2_PLACEMENT_3D ( 'NONE', #18432, #97938, #236190 ) ;
#198962=B_SPLINE_CURVE_WITH_KNOTS ( 'NONE', 3,
 ( #145493, #123379, #24295, #103780, #183358, #4686, #84180, #163796, #243306, #223737, #204179, #25569, #184625, #85486, #12435, #170255, #110217, #112801, #9841, #14997, #192337, #48962, #172816, #150640, #128511, #52805, #30722, #132354, #90648, #91943 ),
 .UNSPECIFIED., .F., .F.,
 ( 4, 2, 2, 2, 2, 2, 2, 2, 2, 2, 2, 2, 2, 2, 4 ),
 ( 0.000000000000000000, 0.0003422764154113199539, 0.0006845528308226399078, 0.001026829246233963927, 0.001369105661645287839, 0.002053658492467965585, 0.002738211323290642898, 0.003080487738701979603, 0.003422764154113315874, 0.003765040569524652145, 0.004107316984935988416, 0.004449593400347324687, 0.004791869815758660958, 0.005134146231169998097, 0.005476422646581333500 ),
 .UNSPECIFIED. ) ;
#198964=CIRCLE ( 'NONE', #119903, 0.09999999999999939493 ) ;
#199028=CARTESIAN_POINT ( 'NONE',  ( -15.15564720441980562, 27.50042447306176285, -233.9693577020172199 ) ) ;
#199129=ORIENTED_EDGE ( 'NONE', *, *, #231093, .T. ) ;
#199254=VECTOR ( 'NONE', #136738, 1000.000000000000000 ) ;
#199370=DIRECTION ( 'NONE',  ( 1.000000000000000000, -1.156482317317869556E-14, -3.083952846180985271E-14 ) ) ;
#199446=CIRCLE ( 'NONE', #74568, 0.1999999999999987899 ) ;
#199818=AXIS2_PLACEMENT_3D ( 'NONE', #149325, #33243, #230119 ) ;
#199877=CARTESIAN_POINT ( 'NONE',  ( 20.27550659511088682, 19.63441466210375808, -229.9765866052221099 ) ) ;
#199931=VECTOR ( 'NONE', #152708, 1000.000000000000000 ) ;
#199990=EDGE_CURVE ( 'NONE', #88287, #40232, #248544, .T. ) ;
#200139=CARTESIAN_POINT ( 'NONE',  ( -18.40000000000000213, 23.82801463864234037, -229.3483719500187306 ) ) ;
#200262=EDGE_CURVE ( 'NONE', #108947, #155129, #139917, .T. ) ;
#200736=DIRECTION ( 'NONE',  ( 1.073024830501117528E-15, -0.8814952561688430555, 0.4721928772777346239 ) ) ;
#200761=DIRECTION ( 'NONE',  ( 1.186688945009009584E-16, -0.4721928772777346239, -0.8814952561688430555 ) ) ;
#201457=CIRCLE ( 'NONE', #197369, 0.1000000000000030864 ) ;
#201558=CARTESIAN_POINT ( 'NONE',  ( 17.74533788810830259, 32.67593350423081233, -235.1446872901578899 ) ) ;
#201780=CARTESIAN_POINT ( 'NONE',  ( -16.86445178670605216, 22.94788858557290467, -230.9050441021552160 ) ) ;
#201830=ORIENTED_EDGE ( 'NONE', *, *, #23501, .T. ) ;
#201970=CARTESIAN_POINT ( 'NONE',  ( -16.93388492042258875, 22.95171134730065887, -230.8772219302610722 ) ) ;
#201986=ORIENTED_EDGE ( 'NONE', *, *, #165004, .T. ) ;
#202192=EDGE_LOOP ( 'NONE', ( #105038, #40752, #244379, #14439 ) ) ;
#202247=ORIENTED_EDGE ( 'NONE', *, *, #92069, .T. ) ;
#202525=LINE ( 'NONE', #103397, #72167 ) ;
#202866=CARTESIAN_POINT ( 'NONE',  ( -12.60829076262180592, 27.26819834643091056, -233.8689871410715853 ) ) ;
#203034=CARTESIAN_POINT ( 'NONE',  ( 23.24999999999999645, 20.83093076766827423, -227.7429161672744442 ) ) ;
#203181=FACE_OUTER_BOUND ( 'NONE', #189353, .T. ) ;
#203220=( BOUNDED_CURVE ( )  B_SPLINE_CURVE ( 3, ( #235305, #94510, #37139, #192343 ),
 .UNSPECIFIED., .F., .F. ) 
 B_SPLINE_CURVE_WITH_KNOTS ( ( 4, 4 ),
 ( 0.3000847527772370071, 0.5497968875596828120 ),
 .UNSPECIFIED. ) 
 CURVE ( )  GEOMETRIC_REPRESENTATION_ITEM ( )  RATIONAL_B_SPLINE_CURVE ( ( 1.000000000000000000, 0.9948104011409417691, 0.9948104011409417691, 1.000000000000000000 ) ) 
 REPRESENTATION_ITEM ( '' )  );
#203508=EDGE_LOOP ( 'NONE', ( #71660, #166102, #37555, #197714 ) ) ;
#203578=ADVANCED_FACE ( 'NONE', ( #141654 ), #103785, .F. ) ;
#203701=CIRCLE ( 'NONE', #178798, 0.1999999999999987899 ) ;
#203712=DIRECTION ( 'NONE',  ( 0.5932847527679308008, -0.3801118060259208176, -0.7095972217059532960 ) ) ;
#203714=CYLINDRICAL_SURFACE ( 'NONE', #224735, 0.5000000000000004441 ) ;
#203749=CARTESIAN_POINT ( 'NONE',  ( -16.83199030136658081, 23.07682551944007443, -231.0099189692009816 ) ) ;
#203782=ORIENTED_EDGE ( 'NONE', *, *, #159180, .T. ) ;
#203831=CARTESIAN_POINT ( 'NONE',  ( -21.65000000000000213, 30.25354784785470486, -234.7188954791831748 ) ) ;
#204076=CARTESIAN_POINT ( 'NONE',  ( -15.15766958671842879, 25.17626390180108231, -232.7245615205268336 ) ) ;
#204179=CARTESIAN_POINT ( 'NONE',  ( 14.88075390448864255, 27.69551741609592455, -234.0500622709107859 ) ) ;
#204200=CARTESIAN_POINT ( 'NONE',  ( -16.89268316805465986, 30.21221237062500720, -234.8082435139909592 ) ) ;
#205035=FACE_OUTER_BOUND ( 'NONE', #69442, .T. ) ;
#205176=ORIENTED_EDGE ( 'NONE', *, *, #165875, .T. ) ;
#205467=DIRECTION ( 'NONE',  ( 0.7071067811865492381, 0.3338907855510725997, 0.6233112732207602980 ) ) ;
#205470=LINE ( 'NONE', #245903, #123147 ) ;
#205548=CIRCLE ( 'NONE', #151431, 0.9000000000000014655 ) ;
#205614=CARTESIAN_POINT ( 'NONE',  ( 18.39999999999999503, 34.05335961020092839, -234.8258093264404636 ) ) ;
#205654=CARTESIAN_POINT ( 'NONE',  ( 13.99999999999999822, 26.54497872210689735, -232.9592037335782209 ) ) ;
#205806=VERTEX_POINT ( 'NONE', #95536 ) ;
#206015=ORIENTED_EDGE ( 'NONE', *, *, #108846, .T. ) ;
#206078=CARTESIAN_POINT ( 'NONE',  ( -18.40000000000000213, 31.17298305880675002, -240.2029303890703886 ) ) ;
#206254=CARTESIAN_POINT ( 'NONE',  ( 21.72449340488910607, 30.36402033568042569, -234.5126641304238149 ) ) ;
#206322=CARTESIAN_POINT ( 'NONE',  ( -16.87683809663753465, 23.48945571633983675, -231.3055249780561837 ) ) ;
#206360=EDGE_LOOP ( 'NONE', ( #3571, #64701, #220651, #12300 ) ) ;
#206385=CARTESIAN_POINT ( 'NONE',  ( -23.25000000000000355, 23.82801463864234037, -229.3483719500187306 ) ) ;
#206426=CARTESIAN_POINT ( 'NONE',  ( -17.01473183483382101, 23.06621698515930063, -230.9822826988503834 ) ) ;
#206456=CARTESIAN_POINT ( 'NONE',  ( -16.94226253665225457, 29.94475842175044988, -234.6669290423084249 ) ) ;
#206527=VECTOR ( 'NONE', #185238, 1000.000000000000000 ) ;
#206552=CARTESIAN_POINT ( 'NONE',  ( -16.77683809663752257, 30.20632856012693424, -234.8070450048000737 ) ) ;
#206679=CARTESIAN_POINT ( 'NONE',  ( -16.78055652883087134, 22.98605849593701578, -230.9430003731122554 ) ) ;
#206840=AXIS2_PLACEMENT_3D ( 'NONE', #15068, #94583, #95859 ) ;
#206852=CARTESIAN_POINT ( 'NONE',  ( -16.94309007106718212, 22.95903659219989024, -230.8769661811952290 ) ) ;
#207549=AXIS2_PLACEMENT_3D ( 'NONE', #233580, #74541, #172361 ) ;
#207600=ORIENTED_EDGE ( 'NONE', *, *, #199990, .F. ) ;
#207652=ORIENTED_EDGE ( 'NONE', *, *, #84236, .F. ) ;
#207876=( BOUNDED_SURFACE ( )  B_SPLINE_SURFACE ( 3, 2, ( 
 ( #37897, #217767, #178704 ),
 ( #79543, #254329, #75729 ),
 ( #18, #177415, #162631 ),
 ( #114841, #135671, #213944 ) ),
 .UNSPECIFIED., .F., .F., .F. ) 
 B_SPLINE_SURFACE_WITH_KNOTS ( ( 4, 4 ),
 ( 3, 3 ),
 ( 5.727910411845712702, 5.983100554402349225 ),
 ( 0.000000000000000000, 1.000000000000000000 ),
 .UNSPECIFIED. ) 
 GEOMETRIC_REPRESENTATION_ITEM ( )  RATIONAL_B_SPLINE_SURFACE ( (
 ( 1.000000000000000000, 0.8946697475932277044, 1.000000000000000000),
 ( 1.000000000000000000, 0.9035312726220163793, 1.000000000000000000),
 ( 1.000000000000000000, 0.9104333467450778095, 1.000000000000000000),
 ( 1.000000000000000000, 0.9152888060719297503, 1.000000000000000000) ) ) 
 REPRESENTATION_ITEM ( '' )  SURFACE ( )  );
#208311=EDGE_LOOP ( 'NONE', ( #169739, #251247, #191570, #233815 ) ) ;
#209002=CARTESIAN_POINT ( 'NONE',  ( -18.40000000000000213, 33.92901942162173157, -235.0579290632217067 ) ) ;
#209027=CARTESIAN_POINT ( 'NONE',  ( -16.92989507731675758, 30.00137997040565097, -234.6972596558748023 ) ) ;
#209067=ORIENTED_EDGE ( 'NONE', *, *, #54675, .T. ) ;
#209267=CARTESIAN_POINT ( 'NONE',  ( 18.39999999999999503, 20.94763808724815846, -234.7254930126486556 ) ) ;
#209451=DIRECTION ( 'NONE',  ( -1.000000000000000000, 0.000000000000000000, -0.000000000000000000 ) ) ;
#209525=FACE_OUTER_BOUND ( 'NONE', #90587, .T. ) ;
#209671=EDGE_LOOP ( 'NONE', ( #1795, #143980, #150506, #28058, #178270, #253183 ) ) ;
#209834=CARTESIAN_POINT ( 'NONE',  ( -18.39999999999999858, 20.76715588789282307, -228.0228088279911560 ) ) ;
#210053=DIRECTION ( 'NONE',  ( 1.000000000000000000, 0.000000000000000000, 0.000000000000000000 ) ) ;
#210150=CARTESIAN_POINT ( 'NONE',  ( -33.72168855820451938, 22.97806745954237684, -230.9350634111225986 ) ) ;
#210318=CARTESIAN_POINT ( 'NONE',  ( -16.77683809663752257, 30.19206623356022234, -234.8041291499450551 ) ) ;
#210325=FACE_OUTER_BOUND ( 'NONE', #157326, .T. ) ;
#210354=DIRECTION ( 'NONE',  ( -0.000000000000000000, 0.8814952561688430555, -0.4721928772777346239 ) ) ;
#210515=AXIS2_PLACEMENT_3D ( 'NONE', #157777, #79451, #244956 ) ;
#210562=( NAMED_UNIT ( * ) SI_UNIT ( $, .STERADIAN. ) SOLID_ANGLE_UNIT ( ) );
#210582=DIRECTION ( 'NONE',  ( -1.000000000000000000, -5.603460673774840016E-17, -1.046060675573451769E-16 ) ) ;
#210700=CARTESIAN_POINT ( 'NONE',  ( -16.94445028196808778, 22.96031635112858282, -230.8778361528912058 ) ) ;
#210861=ORIENTED_EDGE ( 'NONE', *, *, #115411, .T. ) ;
#211025=ORIENTED_EDGE ( 'NONE', *, *, #246962, .F. ) ;
#211050=ORIENTED_EDGE ( 'NONE', *, *, #51930, .F. ) ;
#211357=B_SPLINE_CURVE_WITH_KNOTS ( 'NONE', 3,
 ( #113907, #229999, #153081, #171364, #231306, #250833, #69664, #72231, #151777, #52638 ),
 .UNSPECIFIED., .F., .F.,
 ( 4, 3, 3, 4 ),
 ( 1.960480067105092529E-15, 8.145022132831457041E-06, 1.905645951092260382E-05, 2.061107371225662837E-05 ),
 .UNSPECIFIED. ) ;
#211499=CARTESIAN_POINT ( 'NONE',  ( -18.40000000000000568, 30.89789434349017938, -233.5160218091985200 ) ) ;
#211525=PLANE ( 'NONE',  #236063 ) ;
#211556=AXIS2_PLACEMENT_3D ( 'NONE', #190226, #51966, #154969 ) ;
#211588=EDGE_LOOP ( 'NONE', ( #78826, #4941, #221825, #251750 ) ) ;
#211600=CARTESIAN_POINT ( 'NONE',  ( -16.79140778683512281, 30.18607848682776762, -234.8019360275262102 ) ) ;
#211604=CARTESIAN_POINT ( 'NONE',  ( -16.85722902420145530, 30.10447401013609436, -234.7524843106976107 ) ) ;
#211636=EDGE_CURVE ( 'NONE', #26637, #103956, #226350, .T. ) ;
#211639=CIRCLE ( 'NONE', #207549, 14.30833333333334600 ) ;
#211705=ADVANCED_FACE ( 'NONE', ( #75042 ), #154578, .F. ) ;
#211856=( NAMED_UNIT ( * ) SI_UNIT ( $, .STERADIAN. ) SOLID_ANGLE_UNIT ( ) );
#211884=DIRECTION ( 'NONE',  ( 0.000000000000000000, 0.4721928772777294059, 0.8814952561688458310 ) ) ;
#211991=FACE_OUTER_BOUND ( 'NONE', #212972, .T. ) ;
#212003=CARTESIAN_POINT ( 'NONE',  ( -16.93339986808596365, 22.93003596233614161, -230.8468223696792734 ) ) ;
#212188=CARTESIAN_POINT ( 'NONE',  ( -16.92778301347288661, 30.29959772668862783, -234.7992129936043284 ) ) ;
#212386=FACE_OUTER_BOUND ( 'NONE', #206360, .T. ) ;
#212473=EDGE_CURVE ( 'NONE', #225681, #125503, #143064, .T. ) ;
#212613=CARTESIAN_POINT ( 'NONE',  ( -17.01764560440508944, 30.11817903520203288, -234.7598257174429648 ) ) ;
#212616=CARTESIAN_POINT ( 'NONE',  ( -18.40000000000000213, 31.05627573922685514, -233.2203535436961488 ) ) ;
#212885=CARTESIAN_POINT ( 'NONE',  ( -16.89935556175704079, 29.77468116918558394, -234.5758233140741140 ) ) ;
#212890=DIRECTION ( 'NONE',  ( -0.5932847527679309119, 0.3801118060259214282, 0.7095972217059529630 ) ) ;
#212972=EDGE_LOOP ( 'NONE', ( #90726, #126588, #62352, #205176, #256424, #219780, #226923, #5602, #134722, #84293, #77371, #244262, #74608, #252420, #197022, #111068, #61252, #115826 ) ) ;
#213182=AXIS2_PLACEMENT_3D ( 'NONE', #166624, #66211, #6217 ) ;
#213300=ORIENTED_EDGE ( 'NONE', *, *, #92523, .T. ) ;
#213328=EDGE_CURVE ( 'NONE', #146247, #74153, #211639, .T. ) ;
#213441=ORIENTED_EDGE ( 'NONE', *, *, #30938, .T. ) ;
#213509=CARTESIAN_POINT ( 'NONE',  ( 18.39999999999999503, 34.05335961020092839, -234.8258093264404636 ) ) ;
#213643=EDGE_CURVE ( 'NONE', #25903, #167521, #147300, .T. ) ;
#213654=DIRECTION ( 'NONE',  ( 0.000000000000000000, -0.8814952561688476074, 0.4721928772777262417 ) ) ;
#213944=CARTESIAN_POINT ( 'NONE',  ( -16.87036670365549540, 22.88247411645691543, -230.8391385443351567 ) ) ;
#214091=FACE_OUTER_BOUND ( 'NONE', #23521, .T. ) ;
#214349=CARTESIAN_POINT ( 'NONE',  ( 20.04999999999999716, 19.41435213583508457, -230.3874019357809289 ) ) ;
#214580=CARTESIAN_POINT ( 'NONE',  ( 13.99999999999999822, 26.54497872210689735, -232.9592037335782209 ) ) ;
#214821=( GEOMETRIC_REPRESENTATION_CONTEXT ( 3 ) GLOBAL_UNCERTAINTY_ASSIGNED_CONTEXT ( ( #128645 ) ) GLOBAL_UNIT_ASSIGNED_CONTEXT ( ( #93169, #176587, #210562 ) ) REPRESENTATION_CONTEXT ( 'NONE', 'WORKASPACE' ) );
#215081=CARTESIAN_POINT ( 'NONE',  ( 20.73486653747088226, 21.70314669089255943, -233.3151006027784717 ) ) ;
#215166=CARTESIAN_POINT ( 'NONE',  ( -16.95709691155922982, 30.19746286648991074, -234.8022958954214801 ) ) ;
#215368=CARTESIAN_POINT ( 'NONE',  ( -18.40000000000000213, 33.87871438666832091, -235.0463117791480556 ) ) ;
#215466=CARTESIAN_POINT ( 'NONE',  ( -23.25000000000000355, 20.94763808724815846, -234.7254930126486556 ) ) ;
#215485=EDGE_CURVE ( 'NONE', #231239, #87552, #34486, .T. ) ;
#215658=CARTESIAN_POINT ( 'NONE',  ( -16.84793658983427278, 23.05180160922629895, -230.9745607765919999 ) ) ;
#215669=ADVANCED_FACE ( 'NONE', ( #146377 ), #26469, .F. ) ;
#216383=LINE ( 'NONE', #18193, #2733 ) ;
#216385=B_SPLINE_CURVE_WITH_KNOTS ( 'NONE', 3,
 ( #23374, #1188, #222812, #258055, #101558, #182434, #81994, #239833, #84547, #3781 ),
 .UNSPECIFIED., .F., .F.,
 ( 4, 3, 3, 4 ),
 ( 0.000000000000000000, 1.004626015991573225E-05, 1.831183478183568230E-05, 2.062343583996359216E-05 ),
 .UNSPECIFIED. ) ;
#216478=EDGE_CURVE ( 'NONE', #9149, #88287, #171994, .T. ) ;
#216824=DIRECTION ( 'NONE',  ( 1.186688945009009831E-16, -0.4721928772777346239, -0.8814952561688430555 ) ) ;
#216944=CARTESIAN_POINT ( 'NONE',  ( -16.79270642812283043, 22.98604926797965220, -230.9435997431117187 ) ) ;
#217408=DIRECTION ( 'NONE',  ( -0.7071067811865462405, -0.3338907855510745981, -0.6233112732207625184 ) ) ;
#217519=CARTESIAN_POINT ( 'NONE',  ( -15.55912972643741199, 22.28907679569445932, -232.2212793431121440 ) ) ;
#217698=CARTESIAN_POINT ( 'NONE',  ( 16.87683809663750267, 22.97806745954241592, -230.9350634111226270 ) ) ;
#217767=CARTESIAN_POINT ( 'NONE',  ( -18.41431012584568450, 20.68648449445280235, -227.9633614482561370 ) ) ;
#217880=ORIENTED_EDGE ( 'NONE', *, *, #255652, .F. ) ;
#217954=ORIENTED_EDGE ( 'NONE', *, *, #243883, .T. ) ;
#217957=CARTESIAN_POINT ( 'NONE',  ( 23.04999999999999716, 19.44861527341281615, -230.3234391047226666 ) ) ;
#218098=EDGE_CURVE ( 'NONE', #93310, #31867, #30334, .T. ) ;
#218109=ORIENTED_EDGE ( 'NONE', *, *, #177976, .F. ) ;
#218217=CARTESIAN_POINT ( 'NONE',  ( -16.87401514999228880, 23.03975626714240832, -230.9681084165865173 ) ) ;
#218389=CARTESIAN_POINT ( 'NONE',  ( -16.87036670365549895, 22.95364034536357423, -230.7688863709651628 ) ) ;
#218434=DIRECTION ( 'NONE',  ( -1.000000000000000000, 7.801181613359271466E-16, 1.456333823655509297E-15 ) ) ;
#218671=CARTESIAN_POINT ( 'NONE',  ( -16.90137573187933739, 23.10008176225494481, -231.0004231328723563 ) ) ;
#218788=CARTESIAN_POINT ( 'NONE',  ( -23.25000000000000355, 28.17589918783267322, -238.5974746063260739 ) ) ;
#219057=ORIENTED_EDGE ( 'NONE', *, *, #61764, .F. ) ;
#219246=VERTEX_POINT ( 'NONE', #3939 ) ;
#219475=DIRECTION ( 'NONE',  ( 1.000000000000000000, 0.000000000000000000, 0.000000000000000000 ) ) ;
#219516=CARTESIAN_POINT ( 'NONE',  ( -16.83233564386406655, 23.07933777265768782, -231.0117482525610626 ) ) ;
#219685=DIRECTION ( 'NONE',  ( -1.000000000000000000, 0.000000000000000000, 0.000000000000000000 ) ) ;
#219780=ORIENTED_EDGE ( 'NONE', *, *, #50571, .T. ) ;
#219863=CARTESIAN_POINT ( 'NONE',  ( -15.31895204843005942, 27.34981073572249954, -233.9047583970293545 ) ) ;
#220001=TOROIDAL_SURFACE ( 'NONE', #140908, 14.20833333333334103, 0.1000000000000000056 ) ;
#220042=LINE ( 'NONE', #203034, #72899 ) ;
#220054=FACE_OUTER_BOUND ( 'NONE', #72269, .T. ) ;
#220062=DIRECTION ( 'NONE',  ( -1.000000000000000000, 0.000000000000000000, 0.000000000000000000 ) ) ;
#220164=VERTEX_POINT ( 'NONE', #113802 ) ;
#220175=ORIENTED_EDGE ( 'NONE', *, *, #9294, .T. ) ;
#220190=DIRECTION ( 'NONE',  ( -0.7071067811865486830, 0.3338907855510728218, 0.6233112732207607420 ) ) ;
#220651=ORIENTED_EDGE ( 'NONE', *, *, #135961, .T. ) ;
#220803=CARTESIAN_POINT ( 'NONE',  ( -33.72168855820452649, 33.92263863280957281, -235.0698407953532296 ) ) ;
#221037=DIRECTION ( 'NONE',  ( 0.000000000000000000, -0.8814952561688430555, 0.4721928772777346239 ) ) ;
#221139=CARTESIAN_POINT ( 'NONE',  ( -15.75000000000000711, 26.40960863751540444, -233.4539077120826960 ) ) ;
#221179=CARTESIAN_POINT ( 'NONE',  ( -14.00000000000000178, 26.54497872210690090, -232.9592037335782209 ) ) ;
#221352=CARTESIAN_POINT ( 'NONE',  ( 20.99999999999999645, 30.11188998467138234, -234.9833440560338147 ) ) ;
#221439=PLANE ( 'NONE',  #228782 ) ;
#221825=ORIENTED_EDGE ( 'NONE', *, *, #243883, .F. ) ;
#221996=CARTESIAN_POINT ( 'NONE',  ( -16.83794237512073977, 23.10225113665113383, -231.0284041592679785 ) ) ;
#222017=CARTESIAN_POINT ( 'NONE',  ( 23.04999999999999716, 29.67396024497139706, -235.8008764811443712 ) ) ;
#222154=CARTESIAN_POINT ( 'NONE',  ( 18.54999999999999716, 30.20632856012699108, -234.8070450048000737 ) ) ;
#222380=CARTESIAN_POINT ( 'NONE',  ( 18.39999999999997371, 33.92263863280957281, -235.0698407953532296 ) ) ;
#222443=FACE_OUTER_BOUND ( 'NONE', #111269, .T. ) ;
#222501=VECTOR ( 'NONE', #79580, 1000.000000000000000 ) ;
#222506=EDGE_LOOP ( 'NONE', ( #13012, #242610, #198154, #4271, #20378, #162069 ) ) ;
#222514=CARTESIAN_POINT ( 'NONE',  ( -16.92989143108098204, 23.18300089227618344, -231.0448406408646917 ) ) ;
#222617=AXIS2_PLACEMENT_3D ( 'NONE', #57116, #254048, #213654 ) ;
#222812=CARTESIAN_POINT ( 'NONE',  ( -16.88005004766534967, 30.20667229816764987, -234.8071151212674863 ) ) ;
#223015=EDGE_CURVE ( 'NONE', #171663, #5154, #30538, .T. ) ;
#223072=CARTESIAN_POINT ( 'NONE',  ( 20.04999999999999716, 22.41143600680915426, -231.9928577185252152 ) ) ;
#223349=VECTOR ( 'NONE', #50286, 1000.000000000000000 ) ;
#223523=VERTEX_POINT ( 'NONE', #701 ) ;
#223655=CARTESIAN_POINT ( 'NONE',  ( -33.72168855820452649, 20.70020979027691155, -227.9869476361872103 ) ) ;
#223701=CARTESIAN_POINT ( 'NONE',  ( -12.25000000000000533, 26.41090933635395288, -233.4546044608430293 ) ) ;
#223737=CARTESIAN_POINT ( 'NONE',  ( 15.07585980824113214, 27.57398452308367709, -234.0009067267211833 ) ) ;
#223741=( BOUNDED_SURFACE ( )  B_SPLINE_SURFACE ( 3, 2, ( 
 ( #138114, #78146, #57293 ),
 ( #117295, #97695, #256746 ),
 ( #141978, #19485, #37777 ),
 ( #196815, #40363, #201970 ) ),
 .UNSPECIFIED., .F., .F., .F. ) 
 B_SPLINE_SURFACE_WITH_KNOTS ( ( 4, 4 ),
 ( 3, 3 ),
 ( 4.712388980384689674, 5.765869716888459173 ),
 ( 0.000000000000000000, 1.000000000000000000 ),
 .UNSPECIFIED. ) 
 GEOMETRIC_REPRESENTATION_ITEM ( )  RATIONAL_B_SPLINE_SURFACE ( (
 ( 1.000000000000000000, 0.7071067811865359154, 1.000000000000000000),
 ( 1.000000000000000000, 0.7953136715913566857, 1.000000000000000000),
 ( 1.000000000000000000, 0.8646876308615015772, 1.000000000000000000),
 ( 1.000000000000000000, 0.8984936768950380070, 1.000000000000000000) ) ) 
 REPRESENTATION_ITEM ( '' )  SURFACE ( )  );
#223798=EDGE_CURVE ( 'NONE', #122206, #225681, #199446, .T. ) ;
#223883=CARTESIAN_POINT ( 'NONE',  ( -18.39999999999999858, 20.72457956333081341, -227.9937486218739480 ) ) ;
#224034=CARTESIAN_POINT ( 'NONE',  ( 22.88900146558018989, 19.39258630652192394, -230.4280346437470826 ) ) ;
#224048=ORIENTED_EDGE ( 'NONE', *, *, #240549, .F. ) ;
#224087=EDGE_CURVE ( 'NONE', #101407, #34727, #203701, .T. ) ;
#224292=VECTOR ( 'NONE', #82084, 1000.000000000000000 ) ;
#224403=CARTESIAN_POINT ( 'NONE',  ( -18.40000000000000213, 23.69729366125098480, -229.5924034189314966 ) ) ;
#224486=VECTOR ( 'NONE', #192951, 1000.000000000000000 ) ;
#224497=CARTESIAN_POINT ( 'NONE',  ( -16.80939487329394666, 30.20632856012771583, -234.8070450048004716 ) ) ;
#224625=ORIENTED_EDGE ( 'NONE', *, *, #254006, .F. ) ;
#224680=DIRECTION ( 'NONE',  ( 1.000000000000000000, 6.828358547165751995E-15, 1.501968970420579709E-14 ) ) ;
#224719=LINE ( 'NONE', #125634, #37620 ) ;
#224735=AXIS2_PLACEMENT_3D ( 'NONE', #91475, #52318, #172341 ) ;
#224815=DIRECTION ( 'NONE',  ( 1.000000000000000000, 0.000000000000000000, 0.000000000000000000 ) ) ;
#225032=CARTESIAN_POINT ( 'NONE',  ( -16.91776028072577631, 30.23471468080184721, -234.8070487828878470 ) ) ;
#225299=CARTESIAN_POINT ( 'NONE',  ( -18.34374000495060386, 20.70020979027691155, -227.9869476361872103 ) ) ;
#225681=VERTEX_POINT ( 'NONE', #135503 ) ;
#225977=CARTESIAN_POINT ( 'NONE',  ( -16.93294127766158752, 30.30192492100473700, -234.7978104885644370 ) ) ;
#226350=LINE ( 'NONE', #9889, #223349 ) ;
#226411=ORIENTED_EDGE ( 'NONE', *, *, #4222, .T. ) ;
#226603=CARTESIAN_POINT ( 'NONE',  ( -15.75000000000000355, 26.54497872210690090, -232.9592037335782209 ) ) ;
#226619=CARTESIAN_POINT ( 'NONE',  ( -17.71734398241073905, 32.72136639016480331, -235.1419597067196889 ) ) ;
#226755=CARTESIAN_POINT ( 'NONE',  ( -21.65000000000000213, 23.06621698515930419, -230.9822826988504119 ) ) ;
#226923=ORIENTED_EDGE ( 'NONE', *, *, #23592, .T. ) ;
#227025=CARTESIAN_POINT ( 'NONE',  ( 23.24999999999999645, 31.05627573922685158, -233.2203535436961488 ) ) ;
#227145=B_SPLINE_CURVE_WITH_KNOTS ( 'NONE', 3,
 ( #47664, #144199, #142909, #63381, #162523, #127227, #45119 ),
 .UNSPECIFIED., .F., .F.,
 ( 4, 3, 4 ),
 ( 0.000000000000000000, 4.520325912680593053E-05, 5.794988040901352558E-05 ),
 .UNSPECIFIED. ) ;
#227210=AXIS2_PLACEMENT_3D ( 'NONE', #75584, #19440, #199370 ) ;
#227232=EDGE_CURVE ( 'NONE', #118333, #104609, #98828, .T. ) ;
#227293=CARTESIAN_POINT ( 'NONE',  ( -16.93415306273742260, 30.28081097614087369, -234.7951876594369764 ) ) ;
#227297=CARTESIAN_POINT ( 'NONE',  ( -16.97683809663752186, 29.54312324717475136, -234.4517840742877013 ) ) ;
#227492=CARTESIAN_POINT ( 'NONE',  ( -14.77738660682464378, 24.96400212477831460, -232.5813472152648842 ) ) ;
#227817=VECTOR ( 'NONE', #179659, 1000.000000000000000 ) ;
#227831=DIRECTION ( 'NONE',  ( 1.186688945009009831E-16, -0.4721928772777346239, -0.8814952561688430555 ) ) ;
#227886=CARTESIAN_POINT ( 'NONE',  ( -16.90202395485949793, 30.26058880429625830, -234.8180226659985408 ) ) ;
#227901=EDGE_LOOP ( 'NONE', ( #246141, #107732, #35213, #138574 ) ) ;
#228246=CARTESIAN_POINT ( 'NONE',  ( -18.39999999999999858, 20.83093076766827423, -227.7429161672744442 ) ) ;
#228322=ADVANCED_FACE ( 'NONE', ( #140587 ), #101419, .F. ) ;
#228521=DIRECTION ( 'NONE',  ( -0.7071067811865882069, -0.3338907855510964140, -0.6233112732207032325 ) ) ;
#228782=AXIS2_PLACEMENT_3D ( 'NONE', #239753, #220190, #183632 ) ;
#228991=CARTESIAN_POINT ( 'NONE',  ( -16.93230518875208190, 22.93660538467060661, -230.8552802729159055 ) ) ;
#228995=DIRECTION ( 'NONE',  ( 0.000000000000000000, -0.4721928772777346239, -0.8814952561688430555 ) ) ;
#229272=ADVANCED_FACE ( 'NONE', ( #13328 ), #211525, .F. ) ;
#229529=ORIENTED_EDGE ( 'NONE', *, *, #160121, .F. ) ;
#229634=CARTESIAN_POINT ( 'NONE',  ( -18.40000000000000213, 28.17589918783267322, -238.5974746063260739 ) ) ;
#229670=DIRECTION ( 'NONE',  ( 0.2834754621636357830, -0.9414141221712113428, 0.1827049887871715350 ) ) ;
#229793=DIRECTION ( 'NONE',  ( -1.073024830501118120E-15, 0.8814952561688430555, -0.4721928772777346239 ) ) ;
#229879=CARTESIAN_POINT ( 'NONE',  ( -16.89155683852646561, 29.65330325090004138, -234.5108044860495511 ) ) ;
#229962=DIRECTION ( 'NONE',  ( 0.000000000000000000, -0.4721928772776973204, -0.8814952561688629284 ) ) ;
#229995=CARTESIAN_POINT ( 'NONE',  ( 14.87567385445977131, 25.00761986058639508, -232.6112779818446086 ) ) ;
#229999=CARTESIAN_POINT ( 'NONE',  ( -16.89060415895971090, 22.97504759209065028, -230.9320608734631719 ) ) ;
#230119=DIRECTION ( 'NONE',  ( 1.000000000000000000, 0.000000000000000000, 0.000000000000000000 ) ) ;
#230384=AXIS2_PLACEMENT_3D ( 'NONE', #115059, #236282, #194626 ) ;
#230463=CARTESIAN_POINT ( 'NONE',  ( -23.25000000000000355, 17.95055421627409231, -233.1200372299043693 ) ) ;
#230639=FACE_OUTER_BOUND ( 'NONE', #227901, .T. ) ;
#231006=ADVANCED_FACE ( 'NONE', ( #77119 ), #157989, .F. ) ;
#231014=ORIENTED_EDGE ( 'NONE', *, *, #80736, .F. ) ;
#231093=EDGE_CURVE ( 'NONE', #41838, #5246, #190023, .T. ) ;
#231180=CARTESIAN_POINT ( 'NONE',  ( -16.81931177881023132, 30.13250511629065542, -234.7822519458397039 ) ) ;
#231239=VERTEX_POINT ( 'NONE', #50806 ) ;
#231306=CARTESIAN_POINT ( 'NONE',  ( -16.88219499860498374, 22.97755642726332681, -230.9345554886729985 ) ) ;
#231372=CARTESIAN_POINT ( 'NONE',  ( -12.84409460144754256, 25.17497023110846399, -232.7237055342689303 ) ) ;
#231420=( LENGTH_UNIT ( ) NAMED_UNIT ( * ) SI_UNIT ( .MILLI., .METRE. ) );
#232344=CARTESIAN_POINT ( 'NONE',  ( 23.04999999999999716, 22.44569914438688940, -231.9288948874669529 ) ) ;
#232466=CARTESIAN_POINT ( 'NONE',  ( -16.80621392010898774, 30.16774654306749426, -234.7952233516700176 ) ) ;
#232521=ORIENTED_EDGE ( 'NONE', *, *, #93390, .T. ) ;
#232554=ORIENTED_EDGE ( 'NONE', *, *, #38462, .F. ) ;
#232560=DIRECTION ( 'NONE',  ( -1.000000000000000000, 7.801181613359275410E-16, 1.456333823655510085E-15 ) ) ;
#232753=ORIENTED_EDGE ( 'NONE', *, *, #240549, .T. ) ;
#232802=ADVANCED_FACE ( 'NONE', ( #222443 ), #185914, .F. ) ;
#233220=EDGE_CURVE ( 'NONE', #166513, #118333, #224719, .T. ) ;
#233267=CIRCLE ( 'NONE', #191573, 1.500000000000001332 ) ;
#233295=EDGE_CURVE ( 'NONE', #34034, #167845, #133180, .T. ) ;
#233315=( BOUNDED_CURVE ( )  B_SPLINE_CURVE ( 3, ( #195334, #16686, #175762, #255221 ),
 .UNSPECIFIED., .F., .T. ) 
 B_SPLINE_CURVE_WITH_KNOTS ( ( 4, 4 ),
 ( 1.570796326794908992, 2.617993877991506402 ),
 .UNSPECIFIED. ) 
 CURVE ( )  GEOMETRIC_REPRESENTATION_ITEM ( )  RATIONAL_B_SPLINE_CURVE ( ( 1.000000000000000000, 0.9106836025229592124, 0.9106836025229592124, 1.000000000000000000 ) ) 
 REPRESENTATION_ITEM ( '' )  );
#233580=CARTESIAN_POINT ( 'NONE',  ( -16.77683809663752257, 33.06517536918362055, -220.7872234046467952 ) ) ;
#233589=ORIENTED_EDGE ( 'NONE', *, *, #97443, .F. ) ;
#233677=EDGE_LOOP ( 'NONE', ( #93737, #115111, #126138, #139649 ) ) ;
#233756=CARTESIAN_POINT ( 'NONE',  ( -20.65000000000000568, 20.94763808724815846, -234.7254930126486556 ) ) ;
#233783=( BOUNDED_SURFACE ( )  B_SPLINE_SURFACE ( 3, 2, ( 
 ( #135617, #75677, #176073 ),
 ( #112236, #215166, #113499 ),
 ( #212613, #253003, #255522 ),
 ( #250438, #254273, #173530 ) ),
 .UNSPECIFIED., .F., .F., .T. ) 
 B_SPLINE_SURFACE_WITH_KNOTS ( ( 4, 4 ),
 ( 3, 3 ),
 ( 3.658908243880887756, 4.712388980384689674 ),
 ( 0.000000000000000000, 1.000000000000000000 ),
 .UNSPECIFIED. ) 
 GEOMETRIC_REPRESENTATION_ITEM ( )  RATIONAL_B_SPLINE_SURFACE ( (
 ( 1.000000000000000000, 0.8984936768950779751, 1.000000000000000000),
 ( 1.000000000000000000, 0.8646876308615198958, 1.000000000000000000),
 ( 1.000000000000000000, 0.7953136715913630139, 1.000000000000000000),
 ( 1.000000000000000000, 0.7071067811864313324, 1.000000000000000000) ) ) 
 REPRESENTATION_ITEM ( '' )  SURFACE ( )  );
#233815=ORIENTED_EDGE ( 'NONE', *, *, #213643, .T. ) ;
#233954=CARTESIAN_POINT ( 'NONE',  ( -16.88783316861810135, 23.06821272742414664, -230.9833517633470876 ) ) ;
#234021=DIRECTION ( 'NONE',  ( -1.646408749285563007E-14, 0.4721928772777346239, 0.8814952561688430555 ) ) ;
#234063=DIRECTION ( 'NONE',  ( -0.000000000000000000, 0.8814952561688430555, -0.4721928772777346239 ) ) ;
#234071=DIRECTION ( 'NONE',  ( 0.000000000000000000, 0.8814952561688429444, -0.4721928772777345684 ) ) ;
#234074=CARTESIAN_POINT ( 'NONE',  ( -21.64999999999999858, 23.02528674727019364, -230.8469138855057281 ) ) ;
#234094=CYLINDRICAL_SURFACE ( 'NONE', #206840, 14.30833333333334956 ) ;
#234221=ORIENTED_EDGE ( 'NONE', *, *, #84236, .T. ) ;
#234334=CARTESIAN_POINT ( 'NONE',  ( -16.87368910959167678, 22.95032871809893749, -230.9074151025751860 ) ) ;
#234396=AXIS2_PLACEMENT_3D ( 'NONE', #8763, #252487, #149578 ) ;
#234528=EDGE_CURVE ( 'NONE', #249547, #189014, #160389, .T. ) ;
#234535=CIRCLE ( 'NONE', #192859, 0.1000000000000075273 ) ;
#234548=DIRECTION ( 'NONE',  ( 0.000000000000000000, 0.4721928772777346239, 0.8814952561688430555 ) ) ;
#234634=CARTESIAN_POINT ( 'NONE',  ( -20.65000000000000568, 21.70314669089253812, -233.3151006027785286 ) ) ;
#234949=CARTESIAN_POINT ( 'NONE',  ( -18.40000000000000213, 33.90347449973612015, -235.0533218592931348 ) ) ;
#235174=EDGE_CURVE ( 'NONE', #133539, #42653, #154346, .T. ) ;
#235237=CARTESIAN_POINT ( 'NONE',  ( -16.88705144915384082, 23.22574875786642679, -231.0677395022140672 ) ) ;
#235249=SURFACE_STYLE_FILL_AREA ( #96984 ) ;
#235305=CARTESIAN_POINT ( 'NONE',  ( -16.94107738177415712, 22.92025126680846725, -230.8312174982872591 ) ) ;
#235421=FACE_OUTER_BOUND ( 'NONE', #44537, .T. ) ;
#235617=ORIENTED_EDGE ( 'NONE', *, *, #73368, .T. ) ;
#235697=CARTESIAN_POINT ( 'NONE',  ( -12.25000000000000178, 26.54497872210690090, -232.9592037335782209 ) ) ;
#235825=CARTESIAN_POINT ( 'NONE',  ( -18.40000000000000213, 32.67104411594546320, -237.4063322638886859 ) ) ;
#236063=AXIS2_PLACEMENT_3D ( 'NONE', #147696, #229793, #249375 ) ;
#236190=DIRECTION ( 'NONE',  ( 0.000000000000000000, -0.8814952561688429444, 0.4721928772777345684 ) ) ;
#236198=PRODUCT_DEFINITION_FORMATION_WITH_SPECIFIED_SOURCE ( 'ANY', '', #45061, .NOT_KNOWN. ) ;
#236282=DIRECTION ( 'NONE',  ( -1.000000000000000000, 8.995003028460479049E-16, -4.818376878839538654E-16 ) ) ;
#236334=LINE ( 'NONE', #197204, #186635 ) ;
#236786=VERTEX_POINT ( 'NONE', #60049 ) ;
#236834=ORIENTED_EDGE ( 'NONE', *, *, #141900, .T. ) ;
#236946=ADVANCED_FACE ( 'NONE', ( #32530 ), #11661, .F. ) ;
#237972=ADVANCED_FACE ( 'NONE', ( #15750 ), #109666, .F. ) ;
#238008=EDGE_CURVE ( 'NONE', #117799, #166513, #253035, .T. ) ;
#238249=DIRECTION ( 'NONE',  ( 0.000000000000000000, -0.8814952561688430555, 0.4721928772777346239 ) ) ;
#238327=CARTESIAN_POINT ( 'NONE',  ( 23.24999999999999645, 28.17589918783266967, -238.5974746063260739 ) ) ;
#238834=FACE_OUTER_BOUND ( 'NONE', #168133, .T. ) ;
#238852=AXIS2_PLACEMENT_3D ( 'NONE', #187032, #3208, #166194 ) ;
#239001=LINE ( 'NONE', #210150, #184803 ) ;
#239027=VERTEX_POINT ( 'NONE', #139465 ) ;
#239099=CARTESIAN_POINT ( 'NONE',  ( -16.80891096016313924, 22.96249777872389330, -230.9267231593373424 ) ) ;
#239608=CYLINDRICAL_SURFACE ( 'NONE', #72029, 0.09999999999999560629 ) ;
#239617=EDGE_LOOP ( 'NONE', ( #98506, #150451, #162238, #202247, #167347, #54727 ) ) ;
#239753=CARTESIAN_POINT ( 'NONE',  ( 16.27683809663750125, 19.69766786220171184, -229.8585047820796490 ) ) ;
#239831=( BOUNDED_CURVE ( )  B_SPLINE_CURVE ( 3, ( #186813, #32902, #211499, #189374 ),
 .UNSPECIFIED., .F., .F. ) 
 B_SPLINE_CURVE_WITH_KNOTS ( ( 4, 4 ),
 ( -6.483702463810914196E-14, 1.570796326794903219 ),
 .UNSPECIFIED. ) 
 CURVE ( )  GEOMETRIC_REPRESENTATION_ITEM ( )  RATIONAL_B_SPLINE_CURVE ( ( 1.000000000000000000, 0.8047378541243480621, 0.8047378541243480621, 1.000000000000000000 ) ) 
 REPRESENTATION_ITEM ( '' )  );
#239833=CARTESIAN_POINT ( 'NONE',  ( -16.89146115310546037, 30.21126098987748065, -234.8080499024818266 ) ) ;
#239889=VERTEX_POINT ( 'NONE', #171000 ) ;
#239911=DIRECTION ( 'NONE',  ( -1.652117596168391306E-15, -0.4721928772777346239, -0.8814952561688430555 ) ) ;
#239969=VECTOR ( 'NONE', #50965, 1000.000000000000000 ) ;
#239999=CARTESIAN_POINT ( 'NONE',  ( -18.40000000000000213, 31.01370428745238783, -233.5116043003366713 ) ) ;
#240103=EDGE_CURVE ( 'NONE', #20419, #50994, #15757, .T. ) ;
#240142=CARTESIAN_POINT ( 'NONE',  ( 20.73486653747088582, 18.70606281991848974, -231.7096448200341854 ) ) ;
#240169=LINE ( 'NONE', #181487, #71049 ) ;
#240189=DIRECTION ( 'NONE',  ( 0.000000000000000000, 0.4721928772777346239, 0.8814952561688430555 ) ) ;
#240303=FILL_AREA_STYLE ('',( #57781 ) ) ;
#240322=LINE ( 'NONE', #163352, #156847 ) ;
#240470=ORIENTED_EDGE ( 'NONE', *, *, #251102, .T. ) ;
#240549=EDGE_CURVE ( 'NONE', #167845, #13346, #198964, .T. ) ;
#240723=CARTESIAN_POINT ( 'NONE',  ( -15.73854595235691889, 26.51259657475388920, -233.5074718021644173 ) ) ;
#240827=CARTESIAN_POINT ( 'NONE',  ( -16.97048326478265423, 23.41097584464640136, -231.1669605819007813 ) ) ;
#241588=CARTESIAN_POINT ( 'NONE',  ( -16.78493832629887805, 22.98839712131284685, -230.9453208111997071 ) ) ;
#241754=CARTESIAN_POINT ( 'NONE',  ( -16.87786941232800686, 30.23414331161600899, -234.8126936039916473 ) ) ;
#241997=CARTESIAN_POINT ( 'NONE',  ( -14.22969084473441725, 27.89153536508384335, -234.1274767587460133 ) ) ;
#242191=CARTESIAN_POINT ( 'NONE',  ( -16.92778301347256331, 22.93290994670652694, -230.8530800172858619 ) ) ;
#242224=ORIENTED_EDGE ( 'NONE', *, *, #52700, .F. ) ;
#242610=ORIENTED_EDGE ( 'NONE', *, *, #110961, .T. ) ;
#243177=ORIENTED_EDGE ( 'NONE', *, *, #71146, .T. ) ;
#243202=CARTESIAN_POINT ( 'NONE',  ( -15.75000000000000711, 26.10747769360538229, -233.2920644364424732 ) ) ;
#243268=CARTESIAN_POINT ( 'NONE',  ( -12.42749937872396693, 27.00310224281248495, -233.7483545961832476 ) ) ;
#243306=CARTESIAN_POINT ( 'NONE',  ( 15.31784899511109899, 27.35084141791447010, -233.9052011656356171 ) ) ;
#243553=DIRECTION ( 'NONE',  ( 0.000000000000000000, 0.8814952561688429444, -0.4721928772777345684 ) ) ;
#243571=VERTEX_POINT ( 'NONE', #121303 ) ;
#243883=EDGE_CURVE ( 'NONE', #239889, #20419, #108849, .T. ) ;
#244262=ORIENTED_EDGE ( 'NONE', *, *, #143391, .F. ) ;
#244285=DIRECTION ( 'NONE',  ( 0.000000000000000000, 0.4721928772777346239, 0.8814952561688430555 ) ) ;
#244319=ADVANCED_FACE ( 'NONE', ( #247302 ), #49103, .F. ) ;
#244379=ORIENTED_EDGE ( 'NONE', *, *, #171973, .T. ) ;
#244396=VERTEX_POINT ( 'NONE', #135043 ) ;
#244751=FACE_OUTER_BOUND ( 'NONE', #51162, .T. ) ;
#244956=DIRECTION ( 'NONE',  ( 1.000000000000000000, -9.458662978381124901E-16, 5.066746821047763994E-16 ) ) ;
#245084=VECTOR ( 'NONE', #59832, 1000.000000000000000 ) ;
#245289=VERTEX_POINT ( 'NONE', #191462 ) ;
#245589=CARTESIAN_POINT ( 'NONE',  ( -16.93589915522259304, 30.31383928998786814, -234.7981289524791748 ) ) ;
#245592=CARTESIAN_POINT ( 'NONE',  ( -16.86133551771148831, 30.16343802849835143, -234.7840697211602503 ) ) ;
#245810=CARTESIAN_POINT ( 'NONE',  ( -16.81095280782811230, 22.97806745954164853, -230.9350634111222291 ) ) ;
#245903=CARTESIAN_POINT ( 'NONE',  ( 18.39999999999999503, 31.05627573922685514, -233.2203535436961488 ) ) ;
#245934=ORIENTED_EDGE ( 'NONE', *, *, #161860, .F. ) ;
#246017=ADVANCED_FACE ( 'NONE', ( #251673 ), #73083, .F. ) ;
#246141=ORIENTED_EDGE ( 'NONE', *, *, #151713, .F. ) ;
#246163=EDGE_LOOP ( 'NONE', ( #82208, #235617, #17999, #201830 ) ) ;
#246168=CARTESIAN_POINT ( 'NONE',  ( -16.89797118371380336, 30.29573403885543215, -234.8250098293310941 ) ) ;
#246350=CARTESIAN_POINT ( 'NONE',  ( -18.40000000000000213, 23.60914413563410008, -229.5451841312037402 ) ) ;
#246604=DIRECTION ( 'NONE',  ( -0.000000000000000000, 0.8814952561688430555, -0.4721928772777346239 ) ) ;
#246824=CARTESIAN_POINT ( 'NONE',  ( -16.87683809663752399, 28.30820381385230178, -220.9847017323426144 ) ) ;
#246891=ORIENTED_EDGE ( 'NONE', *, *, #200262, .T. ) ;
#246949=DIRECTION ( 'NONE',  ( -1.073024830501117528E-15, -0.8814952561688430555, 0.4721928772777346239 ) ) ;
#246962=EDGE_CURVE ( 'NONE', #101407, #243571, #240169, .T. ) ;
#247049=CARTESIAN_POINT ( 'NONE',  ( -15.52965525596988705, 25.54511595760794052, -232.9618513057392875 ) ) ;
#247070=CARTESIAN_POINT ( 'NONE',  ( -16.79814274880124358, 22.97986866999201894, -230.9368535240658673 ) ) ;
#247145=AXIS2_PLACEMENT_3D ( 'NONE', #221352, #42735, #100116 ) ;
#247167=EDGE_CURVE ( 'NONE', #111741, #89189, #76921, .T. ) ;
#247302=FACE_OUTER_BOUND ( 'NONE', #239617, .T. ) ;
#247396=CARTESIAN_POINT ( 'NONE',  ( -23.25000000000000355, 20.83093076766827423, -227.7429161672744442 ) ) ;
#248403=DIRECTION ( 'NONE',  ( 0.000000000000000000, 0.4721928772777346239, 0.8814952561688430555 ) ) ;
#248544=LINE ( 'NONE', #145584, #93961 ) ;
#248572=AXIS2_PLACEMENT_3D ( 'NONE', #246824, #128177, #29120 ) ;
#248600=B_SPLINE_CURVE_WITH_KNOTS ( 'NONE', 3,
 ( #210700, #206852, #187305, #9934, #72495, #32090, #67338, #188567, #33389, #86875, #152038, #228991, #30811, #212003, #71210, #8651, #88151, #111607, #12527 ),
 .UNSPECIFIED., .F., .F.,
 ( 4, 3, 3, 3, 3, 3, 4 ),
 ( 0.0001624081864585825768, 0.0001685232196531684422, 0.0001764526673566856301, 0.0001916878551483259131, 0.0002009890782182699649, 0.0002238845907555212563, 0.0002283406619926391719 ),
 .UNSPECIFIED. ) ;
#248697=DIRECTION ( 'NONE',  ( 0.000000000000000000, -0.4721928772777346239, -0.8814952561688430555 ) ) ;
#249035=DIRECTION ( 'NONE',  ( 0.000000000000000000, 0.8814952561688476074, -0.4721928772777262417 ) ) ;
#249197=VECTOR ( 'NONE', #210354, 1000.000000000000000 ) ;
#249373=DIRECTION ( 'NONE',  ( 0.7071067811865463515, 0.3338907855510733769, 0.6233112732207632956 ) ) ;
#249375=DIRECTION ( 'NONE',  ( -1.000000000000000000, -9.458662978381124901E-16, 5.066746821047763994E-16 ) ) ;
#249388=FACE_OUTER_BOUND ( 'NONE', #138282, .T. ) ;
#249544=CARTESIAN_POINT ( 'NONE',  ( 21.72449340488909897, 30.36402033568042924, -234.5126641304238149 ) ) ;
#249547=VERTEX_POINT ( 'NONE', #234074 ) ;
#249666=CARTESIAN_POINT ( 'NONE',  ( -16.77779411503078677, 22.98773664223800139, -230.9446655867606637 ) ) ;
#249675=LINE ( 'NONE', #111438, #36127 ) ;
#249700=EDGE_LOOP ( 'NONE', ( #252547, #190874, #42169, #197462 ) ) ;
#249813=DIRECTION ( 'NONE',  ( 1.000000000000000000, 0.000000000000000000, 0.000000000000000000 ) ) ;
#250015=CARTESIAN_POINT ( 'NONE',  ( -16.91256925476569251, 30.32690185447398790, -234.8310981037861609 ) ) ;
#250071=ORIENTED_EDGE ( 'NONE', *, *, #19684, .T. ) ;
#250438=CARTESIAN_POINT ( 'NONE',  ( -17.11825945287481687, 30.11817903451004952, -234.7598257170722889 ) ) ;
#250455=ORIENTED_EDGE ( 'NONE', *, *, #135961, .F. ) ;
#250664=EDGE_CURVE ( 'NONE', #142779, #123629, #194058, .T. ) ;
#250701=ORIENTED_EDGE ( 'NONE', *, *, #215485, .F. ) ;
#250833=CARTESIAN_POINT ( 'NONE',  ( -16.87851181299898684, 22.97796121983802209, -230.9349578068793676 ) ) ;
#250960=ORIENTED_EDGE ( 'NONE', *, *, #42046, .T. ) ;
#250978=CARTESIAN_POINT ( 'NONE',  ( -23.25000000000000355, 20.94763808724815846, -234.7254930126486556 ) ) ;
#251092=EDGE_LOOP ( 'NONE', ( #209067, #85016, #4259, #233589, #88319 ) ) ;
#251102=EDGE_CURVE ( 'NONE', #31867, #122206, #126713, .T. ) ;
#251247=ORIENTED_EDGE ( 'NONE', *, *, #238008, .T. ) ;
#251284=CARTESIAN_POINT ( 'NONE',  ( -16.89318236219975944, 30.21157524432755537, -234.8081138580095626 ) ) ;
#251366=EDGE_CURVE ( 'NONE', #142779, #253844, #201457, .T. ) ;
#251673=FACE_OUTER_BOUND ( 'NONE', #180147, .T. ) ;
#251750=ORIENTED_EDGE ( 'NONE', *, *, #159180, .F. ) ;
#251755=CARTESIAN_POINT ( 'NONE',  ( 23.24999999999999645, 22.44569914438688940, -231.9288948874669529 ) ) ;
#251862=ORIENTED_EDGE ( 'NONE', *, *, #27763, .T. ) ;
#251921=CARTESIAN_POINT ( 'NONE',  ( -17.27223548796277441, 31.52452514974837783, -235.0646137750854336 ) ) ;
#251994=CARTESIAN_POINT ( 'NONE',  ( -16.93658211146644987, 30.27501720290998222, -234.7938011734946997 ) ) ;
#252042=CYLINDRICAL_SURFACE ( 'NONE', #24094, 0.1999999999999987899 ) ;
#252164=VECTOR ( 'NONE', #94164, 1000.000000000000000 ) ;
#252239=SHAPE_REPRESENTATION_RELATIONSHIP ( 'NONE' , 'NONE' ,  #1804, #1633 ) ;
#252244=AXIS2_PLACEMENT_3D ( 'NONE', #68769, #227831, #4908 ) ;
#252420=ORIENTED_EDGE ( 'NONE', *, *, #216478, .F. ) ;
#252487=DIRECTION ( 'NONE',  ( 0.000000000000000000, -0.4721928772777346239, -0.8814952561688430555 ) ) ;
#252526=EDGE_CURVE ( 'NONE', #104609, #220164, #160651, .T. ) ;
#252547=ORIENTED_EDGE ( 'NONE', *, *, #189190, .F. ) ;
#252578=LINE ( 'NONE', #230463, #134929 ) ;
#252749=CARTESIAN_POINT ( 'NONE',  ( 20.73486653747088582, 28.93140779147706709, -237.1870821964558900 ) ) ;
#252776=CARTESIAN_POINT ( 'NONE',  ( -16.89268316805466341, 22.97380970494227626, -230.9308293615217451 ) ) ;
#252782=EDGE_LOOP ( 'NONE', ( #4056, #47219, #156305 ) ) ;
#252889=CARTESIAN_POINT ( 'NONE',  ( -17.04761207306817283, 30.24242811800702668, -234.7396539225699428 ) ) ;
#253003=CARTESIAN_POINT ( 'NONE',  ( -17.05016517656507347, 30.18632038432621201, -234.7963271727524557 ) ) ;
#253035=LINE ( 'NONE', #229634, #239969 ) ;
#253115=ORIENTED_EDGE ( 'NONE', *, *, #93825, .T. ) ;
#253183=ORIENTED_EDGE ( 'NONE', *, *, #18954, .T. ) ;
#253249=LINE ( 'NONE', #135863, #66643 ) ;
#253476=CARTESIAN_POINT ( 'NONE',  ( -13.12432614554022869, 25.00761986058640929, -232.6112779818446938 ) ) ;
#253652=ORIENTED_EDGE ( 'NONE', *, *, #342, .F. ) ;
#253813=AXIS2_PLACEMENT_3D ( 'NONE', #221179, #142914, #42549 ) ;
#253843=CARTESIAN_POINT ( 'NONE',  ( -16.87683809663752399, 22.93084817181464530, -231.0232129367395260 ) ) ;
#253844=VERTEX_POINT ( 'NONE', #69438 ) ;
#253895=CARTESIAN_POINT ( 'NONE',  ( -16.87036670365549895, 22.88247411645692253, -230.8391385443351282 ) ) ;
#254006=EDGE_CURVE ( 'NONE', #176836, #42537, #146069, .T. ) ;
#254048=DIRECTION ( 'NONE',  ( -1.000000000000000000, 0.000000000000000000, 0.000000000000000000 ) ) ;
#254273=CARTESIAN_POINT ( 'NONE',  ( -17.11825945287481687, 30.20632856012695200, -234.8070450048001021 ) ) ;
#254329=CARTESIAN_POINT ( 'NONE',  ( -17.78241384936779212, 21.28923697791310587, -229.0030853712114549 ) ) ;
#254538=CARTESIAN_POINT ( 'NONE',  ( -16.87401514999240248, 30.14463975252685302, -234.7739999993361266 ) ) ;
#254753=CARTESIAN_POINT ( 'NONE',  ( -16.97683809663752186, 23.64127277249475156, -231.2903243416350847 ) ) ;
#255046=CARTESIAN_POINT ( 'NONE',  ( -18.38204789744325396, 33.92563192663926941, -235.0642528789780101 ) ) ;
#255221=CARTESIAN_POINT ( 'NONE',  ( -16.87331047859649757, 30.20632856012693424, -234.8070450048000737 ) ) ;
#255365=EDGE_CURVE ( 'NONE', #236786, #89147, #198083, .T. ) ;
#255522=CARTESIAN_POINT ( 'NONE',  ( -17.04295772865385672, 30.24169553524738419, -234.7410215167427054 ) ) ;
#255652=EDGE_CURVE ( 'NONE', #253844, #231239, #38385, .T. ) ;
#255939=AXIS2_PLACEMENT_3D ( 'NONE', #199877, #44642, #203712 ) ;
#256424=ORIENTED_EDGE ( 'NONE', *, *, #213328, .T. ) ;
#256488=CARTESIAN_POINT ( 'NONE',  ( 15.48841904831874849, 22.32246587424956985, -232.1589482157900761 ) ) ;
#256508=CARTESIAN_POINT ( 'NONE',  ( -16.27683809663750480, 30.01116235937717391, -235.3831614462291384 ) ) ;
#256746=CARTESIAN_POINT ( 'NONE',  ( -17.04295772865662073, 23.01343443466265271, -230.8690399230656851 ) ) ;
#256766=FACE_OUTER_BOUND ( 'NONE', #144008, .T. ) ;
#257181=EDGE_CURVE ( 'NONE', #170251, #60665, #55563, .T. ) ;
#257224=COLOUR_RGB ( '', 0.31764706, 0.68627451, 0.89019608) ;
#257312=CARTESIAN_POINT ( 'NONE',  ( -16.92280123533723213, 23.15492389264284867, -231.0298005607855032 ) ) ;
#257632=CARTESIAN_POINT ( 'NONE',  ( -16.86578989773640913, 30.32384205394743404, -234.8305042728591161 ) ) ;
#257717=CARTESIAN_POINT ( 'NONE',  ( -16.87036670365549895, 22.88247411645692253, -230.8391385443351282 ) ) ;
#257888=EDGE_LOOP ( 'NONE', ( #149998, #18218, #78654, #18763 ) ) ;
#257996=LINE ( 'NONE', #157716, #173293 ) ;
#258055=CARTESIAN_POINT ( 'NONE',  ( -16.88328101497759448, 30.20753490274668351, -234.8072909416581524 ) ) ;
ENDSEC;
END-ISO-10303-21;
